ISO-10303-21;
HEADER;
FILE_DESCRIPTION (('STEP AP214'),
    '1' );
FILE_NAME ('3. Padlock.step',
    '2026-10-09T08:13:37',
    ( '' ),
    ( '' ),
    'SwSTEP 2.0',
    'SolidWorks 2021',
    '' );
FILE_SCHEMA (( 'AUTOMOTIVE_DESIGN' ));
ENDSEC;

DATA;
#67=FILL_AREA_STYLE ('',( #15655 ) ) ;
#78=VECTOR ( 'NONE', #42057, 1000.000000000000000 ) ;
#216=DIRECTION ( 'NONE',  ( 1.000000000000000000, 0.000000000000000000, -0.000000000000000000 ) ) ;
#219=( LENGTH_UNIT ( ) NAMED_UNIT ( * ) SI_UNIT ( .MILLI., .METRE. ) );
#251=CARTESIAN_POINT ( 'NONE',  ( -10.11618306975752368, 54.14354156754873060, -6.790106699912857202 ) ) ;
#372=CARTESIAN_POINT ( 'NONE',  ( -20.42000000000000881, 0.000000000000000000, -12.50000000000000000 ) ) ;
#396=FILL_AREA_STYLE_COLOUR ( '', #24610 ) ;
#421=ORIENTED_EDGE ( 'NONE', *, *, #43281, .T. ) ;
#443=VERTEX_POINT ( 'NONE', #33210 ) ;
#468=( NAMED_UNIT ( * ) SI_UNIT ( $, .STERADIAN. ) SOLID_ANGLE_UNIT ( ) );
#511=FILL_AREA_STYLE_COLOUR ( '', #37228 ) ;
#527=ORIENTED_EDGE ( 'NONE', *, *, #58530, .F. ) ;
#538=CARTESIAN_POINT ( 'NONE',  ( 6.999798566743343997, 9.396926207859090496, -11.50901484383455120 ) ) ;
#604=ORIENTED_EDGE ( 'NONE', *, *, #23658, .F. ) ;
#661=( GEOMETRIC_REPRESENTATION_CONTEXT ( 3 ) GLOBAL_UNCERTAINTY_ASSIGNED_CONTEXT ( ( #46852 ) ) GLOBAL_UNIT_ASSIGNED_CONTEXT ( ( #30764, #11314, #10968 ) ) REPRESENTATION_CONTEXT ( 'NONE', 'WORKASPACE' ) );
#662=ADVANCED_FACE ( 'NONE', ( #5583 ), #47541, .F. ) ;
#789=SURFACE_SIDE_STYLE ('',( #20956 ) ) ;
#852=ORIENTED_EDGE ( 'NONE', *, *, #10725, .F. ) ;
#920=CARTESIAN_POINT ( 'NONE',  ( 0.000000000000000000, 0.000000000000000000, 12.50000000000000000 ) ) ;
#947=CARTESIAN_POINT ( 'NONE',  ( -17.41059898028469277, 6.938893903907228378E-15, 12.50000000000000000 ) ) ;
#1039=COLOUR_RGB ( '', 0.31764706, 0.68627451, 0.89019608) ;
#1136=ADVANCED_FACE ( 'NONE', ( #6215 ), #44928, .F. ) ;
#1341=PRESENTATION_STYLE_ASSIGNMENT (( #44369 ) ) ;
#1424=COLOUR_RGB ( '', 0.66274510, 0.83137255, 0.94901961) ;
#1465=CARTESIAN_POINT ( 'NONE',  ( -13.23915246117191025, 52.65078610323165265, 12.50000000000000000 ) ) ;
#1469=MECHANICAL_DESIGN_GEOMETRIC_PRESENTATION_REPRESENTATION('',(#16174),#3746);
#1508=CARTESIAN_POINT ( 'NONE',  ( 3.999798566743339556, 8.867945265733707672, 12.50000000000000000 ) ) ;
#1540=STYLED_ITEM ( 'NONE', ( #33585 ), #31183 ) ;
#1561=DIRECTION ( 'NONE',  ( 0.9968761159932768567, -0.07898106964430656740, 0.000000000000000000 ) ) ;
#1584=DIRECTION ( 'NONE',  ( 0.07854820085872894764, 0.9914125719358882760, 0.1045528208578022367 ) ) ;
#1666=ORIENTED_EDGE ( 'NONE', *, *, #5331, .T. ) ;
#1680=VERTEX_POINT ( 'NONE', #372 ) ;
#1691=ORIENTED_EDGE ( 'NONE', *, *, #43453, .F. ) ;
#1716=VECTOR ( 'NONE', #36325, 1000.000000000000000 ) ;
#1781=FILL_AREA_STYLE ('',( #28545 ) ) ;
#2088=AXIS2_PLACEMENT_3D ( 'NONE', #37026, #10260, #26413 ) ;
#2090=EDGE_CURVE ( 'NONE', #9321, #29580, #50189, .T. ) ;
#2100=ORIENTED_EDGE ( 'NONE', *, *, #3711, .T. ) ;
#2111=( NAMED_UNIT ( * ) SI_UNIT ( $, .STERADIAN. ) SOLID_ANGLE_UNIT ( ) );
#2123=DIRECTION ( 'NONE',  ( -0.07898106964430649801, -0.9968761159932768567, -1.346643164337371088E-16 ) ) ;
#2164=EDGE_CURVE ( 'NONE', #42390, #22827, #66432, .T. ) ;
#2174=VECTOR ( 'NONE', #51707, 1000.000000000000000 ) ;
#2230=EDGE_CURVE ( 'NONE', #18730, #36574, #67390, .T. ) ;
#2308=VECTOR ( 'NONE', #50991, 1000.000000000000000 ) ;
#2318=ADVANCED_FACE ( 'NONE', ( #65542 ), #54961, .F. ) ;
#2399=VERTEX_POINT ( 'NONE', #46211 ) ;
#2408=ORIENTED_EDGE ( 'NONE', *, *, #26432, .F. ) ;
#2472=( NAMED_UNIT ( * ) PLANE_ANGLE_UNIT ( ) SI_UNIT ( $, .RADIAN. ) );
#2509=LINE ( 'NONE', #1465, #48886 ) ;
#2549=( GEOMETRIC_REPRESENTATION_CONTEXT ( 3 ) GLOBAL_UNCERTAINTY_ASSIGNED_CONTEXT ( ( #54525 ) ) GLOBAL_UNIT_ASSIGNED_CONTEXT ( ( #17244, #60112, #23186 ) ) REPRESENTATION_CONTEXT ( 'NONE', 'WORKASPACE' ) );
#2580=ORIENTED_EDGE ( 'NONE', *, *, #45397, .T. ) ;
#2599=DIRECTION ( 'NONE',  ( 1.000000000000000000, 0.000000000000000000, 0.000000000000000000 ) ) ;
#2615=VERTEX_POINT ( 'NONE', #33459 ) ;
#2617=SURFACE_STYLE_FILL_AREA ( #61388 ) ;
#2664=LINE ( 'NONE', #29064, #57048 ) ;
#2730=FACE_OUTER_BOUND ( 'NONE', #20690, .T. ) ;
#2747=VECTOR ( 'NONE', #17503, 1000.000000000000114 ) ;
#2786=CIRCLE ( 'NONE', #42212, 2.000000000000003553 ) ;
#2830=( NAMED_UNIT ( * ) PLANE_ANGLE_UNIT ( ) SI_UNIT ( $, .RADIAN. ) );
#2836=CARTESIAN_POINT ( 'NONE',  ( -0.000000000000000000, 8.270287287112621792E-15, -12.50000000000000000 ) ) ;
#2857=ORIENTED_EDGE ( 'NONE', *, *, #58792, .F. ) ;
#2874=DIRECTION ( 'NONE',  ( -1.000000000000000000, 0.000000000000000000, 0.000000000000000000 ) ) ;
#2892=ORIENTED_EDGE ( 'NONE', *, *, #13497, .F. ) ;
#3007=SURFACE_SIDE_STYLE ('',( #13967 ) ) ;
#3062=DIRECTION ( 'NONE',  ( -1.000000000000000000, 0.000000000000000000, 0.000000000000000000 ) ) ;
#3089=FILL_AREA_STYLE ('',( #29885 ) ) ;
#3111=( NAMED_UNIT ( * ) SI_UNIT ( $, .STERADIAN. ) SOLID_ANGLE_UNIT ( ) );
#3117=VERTEX_POINT ( 'NONE', #40396 ) ;
#3198=( BOUNDED_CURVE ( )  B_SPLINE_CURVE ( 3, ( #64947, #61730, #34664, #3312 ),
 .UNSPECIFIED., .F., .F. ) 
 B_SPLINE_CURVE_WITH_KNOTS ( ( 4, 4 ),
 ( 5.683226373146454513, 6.380992534147263306 ),
 .UNSPECIFIED. ) 
 CURVE ( )  GEOMETRIC_REPRESENTATION_ITEM ( )  RATIONAL_B_SPLINE_CURVE ( ( 1.000000000000000000, 0.9598367440515259696, 0.9598367440515259696, 1.000000000000000000 ) ) 
 REPRESENTATION_ITEM ( '' )  );
#3279=ORIENTED_EDGE ( 'NONE', *, *, #62754, .F. ) ;
#3305=SURFACE_STYLE_USAGE ( .BOTH. , #30407 ) ;
#3308=ORIENTED_EDGE ( 'NONE', *, *, #16322, .F. ) ;
#3312=CARTESIAN_POINT ( 'NONE',  ( 1.804495846578303864, 51.08602766979955589, -7.112547338523483198 ) ) ;
#3359=ADVANCED_FACE ( 'NONE', ( #38616 ), #66690, .F. ) ;
#3391=PLANE ( 'NONE',  #63243 ) ;
#3402=EDGE_CURVE ( 'NONE', #46838, #22827, #41632, .T. ) ;
#3437=VERTEX_POINT ( 'NONE', #40312 ) ;
#3452=STYLED_ITEM ( 'NONE', ( #39977 ), #35029 ) ;
#3522=SURFACE_STYLE_FILL_AREA ( #62315 ) ;
#3578=AXIS2_PLACEMENT_3D ( 'NONE', #18084, #29678, #34592 ) ;
#3588=EDGE_LOOP ( 'NONE', ( #421, #68397 ) ) ;
#3650=( NAMED_UNIT ( * ) PLANE_ANGLE_UNIT ( ) SI_UNIT ( $, .RADIAN. ) );
#3711=EDGE_CURVE ( 'NONE', #26409, #21935, #24295, .T. ) ;
#3722=DIRECTION ( 'NONE',  ( -0.000000000000000000, -0.000000000000000000, -1.000000000000000000 ) ) ;
#3746=( GEOMETRIC_REPRESENTATION_CONTEXT ( 3 ) GLOBAL_UNCERTAINTY_ASSIGNED_CONTEXT ( ( #56473 ) ) GLOBAL_UNIT_ASSIGNED_CONTEXT ( ( #17388, #22637, #38520 ) ) REPRESENTATION_CONTEXT ( 'NONE', 'WORKASPACE' ) );
#3747=LINE ( 'NONE', #35799, #65566 ) ;
#3771=( NAMED_UNIT ( * ) PLANE_ANGLE_UNIT ( ) SI_UNIT ( $, .RADIAN. ) );
#3876=COLOUR_RGB ( '', 0.08235294, 0.09019608, 0.10196078) ;
#3890=EDGE_CURVE ( 'NONE', #3437, #13821, #34503, .T. ) ;
#3931=STYLED_ITEM ( 'NONE', ( #53860 ), #56708 ) ;
#4018=VERTEX_POINT ( 'NONE', #23188 ) ;
#4110=ORIENTED_EDGE ( 'NONE', *, *, #22794, .F. ) ;
#4152=ORIENTED_EDGE ( 'NONE', *, *, #25563, .F. ) ;
#4217=LINE ( 'NONE', #41567, #38564 ) ;
#4219=ORIENTED_EDGE ( 'NONE', *, *, #13410, .T. ) ;
#4235=AXIS2_PLACEMENT_3D ( 'NONE', #30003, #57084, #7514 ) ;
#4267=ORIENTED_EDGE ( 'NONE', *, *, #55376, .F. ) ;
#4271=CARTESIAN_POINT ( 'NONE',  ( 8.256904162901426147, 56.03086067945960735, 6.591072975109653953 ) ) ;
#4310=DIRECTION ( 'NONE',  ( -0.000000000000000000, -0.000000000000000000, 1.000000000000000000 ) ) ;
#4340=AXIS2_PLACEMENT_3D ( 'NONE', #10749, #11422, #37878 ) ;
#4356=CARTESIAN_POINT ( 'NONE',  ( -10.11618306975752368, 54.14354156754873060, 6.790106699912857202 ) ) ;
#4369=DIRECTION ( 'NONE',  ( 1.000000000000000000, 0.000000000000000000, 0.000000000000000000 ) ) ;
#4403=UNCERTAINTY_MEASURE_WITH_UNIT (LENGTH_MEASURE( 1.000000000000000082E-05 ), #53576, 'distance_accuracy_value', 'NONE');
#4420=DIRECTION ( 'NONE',  ( -1.000000000000000000, 0.000000000000000000, 0.000000000000000000 ) ) ;
#4449=UNCERTAINTY_MEASURE_WITH_UNIT (LENGTH_MEASURE( 1.000000000000000082E-05 ), #34662, 'distance_accuracy_value', 'NONE');
#4508=SURFACE_STYLE_FILL_AREA ( #8775 ) ;
#4521=ORIENTED_EDGE ( 'NONE', *, *, #16322, .T. ) ;
#4612=EDGE_CURVE ( 'NONE', #29580, #6296, #16391, .T. ) ;
#4653=AXIS2_PLACEMENT_3D ( 'NONE', #51197, #50844, #2599 ) ;
#4706=CARTESIAN_POINT ( 'NONE',  ( 6.999798566743346662, 9.396926207859090496, 12.50000000000000000 ) ) ;
#4731=CARTESIAN_POINT ( 'NONE',  ( -13.23915246117191025, 52.65078610323165265, 6.947530358905294356 ) ) ;
#4743=ORIENTED_EDGE ( 'NONE', *, *, #25562, .T. ) ;
#4788=CARTESIAN_POINT ( 'NONE',  ( 3.999798566743339556, 8.867945265733707672, 2.000000000000000000 ) ) ;
#4819=EDGE_LOOP ( 'NONE', ( #4743, #52373, #64686, #65728 ) ) ;
#4909=SURFACE_STYLE_USAGE ( .BOTH. , #37674 ) ;
#4914=CARTESIAN_POINT ( 'NONE',  ( -0.000000000000000000, 8.270287287112621792E-15, -12.50000000000000000 ) ) ;
#4987=ORIENTED_EDGE ( 'NONE', *, *, #12057, .T. ) ;
#5204=FILL_AREA_STYLE_COLOUR ( '', #42865 ) ;
#5211=EDGE_CURVE ( 'NONE', #42181, #69289, #11154, .T. ) ;
#5252=DIRECTION ( 'NONE',  ( -0.000000000000000000, 0.000000000000000000, 1.000000000000000000 ) ) ;
#5278=( NAMED_UNIT ( * ) PLANE_ANGLE_UNIT ( ) SI_UNIT ( $, .RADIAN. ) );
#5331=EDGE_CURVE ( 'NONE', #44875, #43499, #2786, .T. ) ;
#5355=ORIENTED_EDGE ( 'NONE', *, *, #45159, .F. ) ;
#5505=EDGE_LOOP ( 'NONE', ( #53290, #17646, #51894, #42608 ) ) ;
#5507=DIRECTION ( 'NONE',  ( 1.000000000000000000, 0.000000000000000000, 0.000000000000000000 ) ) ;
#5583=FACE_OUTER_BOUND ( 'NONE', #20380, .T. ) ;
#5585=PRESENTATION_STYLE_ASSIGNMENT (( #59073 ) ) ;
#5625=( GEOMETRIC_REPRESENTATION_CONTEXT ( 3 ) GLOBAL_UNCERTAINTY_ASSIGNED_CONTEXT ( ( #57298 ) ) GLOBAL_UNIT_ASSIGNED_CONTEXT ( ( #219, #48522, #6257 ) ) REPRESENTATION_CONTEXT ( 'NONE', 'WORKASPACE' ) );
#5716=MECHANICAL_DESIGN_GEOMETRIC_PRESENTATION_REPRESENTATION('',(#49440),#32693);
#5834=FACE_OUTER_BOUND ( 'NONE', #15264, .T. ) ;
#5928=SURFACE_STYLE_USAGE ( .BOTH. , #22126 ) ;
#5945=PRESENTATION_STYLE_ASSIGNMENT (( #6622 ) ) ;
#5955=VECTOR ( 'NONE', #47548, 1000.000000000000000 ) ;
#5965=STYLED_ITEM ( 'NONE', ( #39439 ), #29512 ) ;
#5977=DIRECTION ( 'NONE',  ( 0.000000000000000000, 1.000000000000000000, 1.734723475976805615E-16 ) ) ;
#5991=LINE ( 'NONE', #21841, #24689 ) ;
#6007=COLOUR_RGB ( '', 0.31764706, 0.68627451, 0.89019608) ;
#6036=DIRECTION ( 'NONE',  ( 0.000000000000000000, -1.000000000000000000, 1.350863103983176297E-16 ) ) ;
#6112=LINE ( 'NONE', #46574, #60828 ) ;
#6154=CARTESIAN_POINT ( 'NONE',  ( -15.79964225816357626, 58.31681314173472686, 6.349999999999996092 ) ) ;
#6215=FACE_OUTER_BOUND ( 'NONE', #15532, .T. ) ;
#6257=( NAMED_UNIT ( * ) SI_UNIT ( $, .STERADIAN. ) SOLID_ANGLE_UNIT ( ) );
#6266=CYLINDRICAL_SURFACE ( 'NONE', #21889, 15.00000000000000000 ) ;
#6269=SURFACE_SIDE_STYLE ('',( #58708 ) ) ;
#6296=VERTEX_POINT ( 'NONE', #16621 ) ;
#6376=CARTESIAN_POINT ( 'NONE',  ( 3.062992266794108520, 51.20951172609373003, 7.099524902877636379 ) ) ;
#6404=ORIENTED_EDGE ( 'NONE', *, *, #5211, .T. ) ;
#6416=SURFACE_STYLE_USAGE ( .BOTH. , #43757 ) ;
#6485=PLANE ( 'NONE',  #8341 ) ;
#6622=SURFACE_STYLE_USAGE ( .BOTH. , #38364 ) ;
#6645=( NAMED_UNIT ( * ) SI_UNIT ( $, .STERADIAN. ) SOLID_ANGLE_UNIT ( ) );
#6687=MECHANICAL_DESIGN_GEOMETRIC_PRESENTATION_REPRESENTATION('',(#19032),#34754);
#6698=ORIENTED_EDGE ( 'NONE', *, *, #37794, .T. ) ;
#6735=CYLINDRICAL_SURFACE ( 'NONE', #24849, 5.000000000000000000 ) ;
#6748=CIRCLE ( 'NONE', #48373, 2.000000000000003553 ) ;
#6784=EDGE_LOOP ( 'NONE', ( #59652, #48217, #48883, #67476, #11572, #20565, #68242, #39945 ) ) ;
#6847=EDGE_CURVE ( 'NONE', #51899, #44849, #3747, .T. ) ;
#6918=CARTESIAN_POINT ( 'NONE',  ( 8.319377385370872346, -3.000000000000000888, 2.000000000000000000 ) ) ;
#6942=EDGE_CURVE ( 'NONE', #34386, #443, #19613, .T. ) ;
#6979=FACE_OUTER_BOUND ( 'NONE', #47446, .T. ) ;
#7033=DIRECTION ( 'NONE',  ( 1.000000000000000000, 0.000000000000000000, 0.000000000000000000 ) ) ;
#7096=VECTOR ( 'NONE', #45730, 1000.000000000000000 ) ;
#7102=ORIENTED_EDGE ( 'NONE', *, *, #53904, .T. ) ;
#7112=EDGE_LOOP ( 'NONE', ( #27139, #13434, #17810, #5355 ) ) ;
#7115=PLANE ( 'NONE',  #29155 ) ;
#7126=( NAMED_UNIT ( * ) SI_UNIT ( $, .STERADIAN. ) SOLID_ANGLE_UNIT ( ) );
#7156=ORIENTED_EDGE ( 'NONE', *, *, #18874, .F. ) ;
#7198=VECTOR ( 'NONE', #15345, 999.9999999999998863 ) ;
#7212=ORIENTED_EDGE ( 'NONE', *, *, #55617, .F. ) ;
#7217=DIRECTION ( 'NONE',  ( 0.000000000000000000, 0.000000000000000000, 1.000000000000000000 ) ) ;
#7231=ADVANCED_FACE ( 'NONE', ( #39994 ), #34657, .T. ) ;
#7292=EDGE_CURVE ( 'NONE', #443, #59509, #42097, .T. ) ;
#7367=LINE ( 'NONE', #55887, #31686 ) ;
#7406=ORIENTED_EDGE ( 'NONE', *, *, #33745, .T. ) ;
#7445=DIRECTION ( 'NONE',  ( -0.000000000000000000, -0.000000000000000000, 1.000000000000000000 ) ) ;
#7504=COLOUR_RGB ( '', 0.09019608, 0.27058824, 0.51372549) ;
#7514=DIRECTION ( 'NONE',  ( 0.000000000000000000, -1.000000000000000000, 1.734723475976805615E-16 ) ) ;
#7587=ORIENTED_EDGE ( 'NONE', *, *, #28974, .F. ) ;
#7683=PRODUCT_DEFINITION ( 'UNKNOWN', '', #14680, #29713 ) ;
#7719=CARTESIAN_POINT ( 'NONE',  ( 0.000000000000000000, 0.000000000000000000, -12.50000000000000000 ) ) ;
#7784=ORIENTED_EDGE ( 'NONE', *, *, #51887, .T. ) ;
#7803=( GEOMETRIC_REPRESENTATION_CONTEXT ( 3 ) GLOBAL_UNCERTAINTY_ASSIGNED_CONTEXT ( ( #4403 ) ) GLOBAL_UNIT_ASSIGNED_CONTEXT ( ( #53576, #63777, #15623 ) ) REPRESENTATION_CONTEXT ( 'NONE', 'WORKASPACE' ) );
#7921=( NAMED_UNIT ( * ) SI_UNIT ( $, .STERADIAN. ) SOLID_ANGLE_UNIT ( ) );
#7929=SURFACE_STYLE_FILL_AREA ( #34651 ) ;
#7987=DIRECTION ( 'NONE',  ( 1.000000000000000000, -0.000000000000000000, -0.000000000000000000 ) ) ;
#8046=ORIENTED_EDGE ( 'NONE', *, *, #2090, .T. ) ;
#8053=CARTESIAN_POINT ( 'NONE',  ( -13.23915246117191025, 52.65078610323165265, 2.000000000000000000 ) ) ;
#8066=( NAMED_UNIT ( * ) PLANE_ANGLE_UNIT ( ) SI_UNIT ( $, .RADIAN. ) );
#8087=( NAMED_UNIT ( * ) PLANE_ANGLE_UNIT ( ) SI_UNIT ( $, .RADIAN. ) );
#8091=( BOUNDED_CURVE ( )  B_SPLINE_CURVE ( 3, ( #23524, #55891, #24549, #45035 ),
 .UNSPECIFIED., .F., .F. ) 
 B_SPLINE_CURVE_WITH_KNOTS ( ( 4, 4 ),
 ( 5.683226373146454513, 6.380992534147263306 ),
 .UNSPECIFIED. ) 
 CURVE ( )  GEOMETRIC_REPRESENTATION_ITEM ( )  RATIONAL_B_SPLINE_CURVE ( ( 1.000000000000000000, 0.9598367440515259696, 0.9598367440515259696, 1.000000000000000000 ) ) 
 REPRESENTATION_ITEM ( '' )  );
#8105=EDGE_CURVE ( 'NONE', #31257, #4018, #14938, .T. ) ;
#8111=CARTESIAN_POINT ( 'NONE',  ( 9.212945446956389617, 3.316355128537251229, 12.15026236960284400 ) ) ;
#8125=UNCERTAINTY_MEASURE_WITH_UNIT (LENGTH_MEASURE( 1.000000000000000082E-05 ), #40651, 'distance_accuracy_value', 'NONE');
#8145=SURFACE_SIDE_STYLE ('',( #34181 ) ) ;
#8171=DIRECTION ( 'NONE',  ( -0.000000000000000000, -0.000000000000000000, 1.000000000000000000 ) ) ;
#8185=EDGE_CURVE ( 'NONE', #2399, #60757, #8091, .T. ) ;
#8199=DIRECTION ( 'NONE',  ( -0.07898106964430656740, -0.9968761159932768567, 0.000000000000000000 ) ) ;
#8272=PLANE ( 'NONE',  #21493 ) ;
#8311=SURFACE_STYLE_FILL_AREA ( #59304 ) ;
#8341=AXIS2_PLACEMENT_3D ( 'NONE', #8519, #55022, #66913 ) ;
#8345=COLOUR_RGB ( '', 0.09019608, 0.27058824, 0.51372549) ;
#8355=AXIS2_PLACEMENT_3D ( 'NONE', #13204, #41371, #13917 ) ;
#8420=( GEOMETRIC_REPRESENTATION_CONTEXT ( 3 ) GLOBAL_UNCERTAINTY_ASSIGNED_CONTEXT ( ( #52403 ) ) GLOBAL_UNIT_ASSIGNED_CONTEXT ( ( #26838, #64159, #43112 ) ) REPRESENTATION_CONTEXT ( 'NONE', 'WORKASPACE' ) );
#8519=CARTESIAN_POINT ( 'NONE',  ( 3.999798566743339556, 8.867945265733707672, -2.000000000000000000 ) ) ;
#8532=AXIS2_PLACEMENT_3D ( 'NONE', #59396, #48216, #21434 ) ;
#8617=FILL_AREA_STYLE ('',( #51510 ) ) ;
#8631=SURFACE_STYLE_FILL_AREA ( #18493 ) ;
#8645=PRESENTATION_STYLE_ASSIGNMENT (( #3305 ) ) ;
#8672=AXIS2_PLACEMENT_3D ( 'NONE', #62766, #51901, #6036 ) ;
#8697=FILL_AREA_STYLE_COLOUR ( '', #8345 ) ;
#8727=DIRECTION ( 'NONE',  ( 0.000000000000000000, 1.000000000000000000, 0.000000000000000000 ) ) ;
#8740=VERTEX_POINT ( 'NONE', #6154 ) ;
#8772=CARTESIAN_POINT ( 'NONE',  ( 17.15973193263811680, -3.000000000000000000, 12.50000000000000000 ) ) ;
#8775=FILL_AREA_STYLE ('',( #25291 ) ) ;
#8790=EDGE_LOOP ( 'NONE', ( #24170, #2580, #11051, #14207 ) ) ;
#8800=SURFACE_STYLE_FILL_AREA ( #57327 ) ;
#8809=UNCERTAINTY_MEASURE_WITH_UNIT (LENGTH_MEASURE( 1.000000000000000082E-05 ), #68078, 'distance_accuracy_value', 'NONE');
#8850=DIRECTION ( 'NONE',  ( -0.000000000000000000, -0.000000000000000000, -1.000000000000000000 ) ) ;
#8957=PRESENTATION_STYLE_ASSIGNMENT (( #24759 ) ) ;
#9028=CARTESIAN_POINT ( 'NONE',  ( -1.953228634907021810, 72.00000000000001421, 12.50000000000000000 ) ) ;
#9046=( NAMED_UNIT ( * ) SI_UNIT ( $, .STERADIAN. ) SOLID_ANGLE_UNIT ( ) );
#9069=STYLED_ITEM ( 'NONE', ( #43262 ), #59678 ) ;
#9153=ORIENTED_EDGE ( 'NONE', *, *, #3402, .T. ) ;
#9164=( NAMED_UNIT ( * ) PLANE_ANGLE_UNIT ( ) SI_UNIT ( $, .RADIAN. ) );
#9207=DIRECTION ( 'NONE',  ( 1.000000000000000000, 0.000000000000000000, 0.000000000000000000 ) ) ;
#9309=CARTESIAN_POINT ( 'NONE',  ( 3.999798566743339556, 8.867945265733707672, -2.000000000000000000 ) ) ;
#9321=VERTEX_POINT ( 'NONE', #67021 ) ;
#9365=EDGE_CURVE ( 'NONE', #60568, #63828, #32469, .T. ) ;
#9402=MECHANICAL_DESIGN_GEOMETRIC_PRESENTATION_REPRESENTATION('',(#18386),#13902);
#9432=FACE_OUTER_BOUND ( 'NONE', #60566, .T. ) ;
#9488=EDGE_CURVE ( 'NONE', #8740, #3437, #11729, .T. ) ;
#9584=LINE ( 'NONE', #24333, #39340 ) ;
#9639=VECTOR ( 'NONE', #54742, 1000.000000000000114 ) ;
#9674=CARTESIAN_POINT ( 'NONE',  ( 10.42000000000000348, -1.224646799147353651E-15, 12.50000000000000000 ) ) ;
#9741=EDGE_LOOP ( 'NONE', ( #34080, #61254 ) ) ;
#9772=STYLED_ITEM ( 'NONE', ( #12504 ), #3359 ) ;
#9782=FILL_AREA_STYLE_COLOUR ( '', #1424 ) ;
#9828=FILL_AREA_STYLE ('',( #5204 ) ) ;
#9905=CARTESIAN_POINT ( 'NONE',  ( -13.23915246117191025, 52.65078610323165265, -2.000000000000000000 ) ) ;
#10043=EDGE_LOOP ( 'NONE', ( #42400, #54838, #30829, #39184, #25089 ) ) ;
#10161=PRESENTATION_STYLE_ASSIGNMENT (( #43258 ) ) ;
#10178=CIRCLE ( 'NONE', #30373, 5.000000000000004441 ) ;
#10196=ORIENTED_EDGE ( 'NONE', *, *, #55376, .T. ) ;
#10211=DIRECTION ( 'NONE',  ( 0.000000000000000000, 0.000000000000000000, 1.000000000000000000 ) ) ;
#10260=DIRECTION ( 'NONE',  ( 0.000000000000000000, 1.350863103983176297E-16, 1.000000000000000000 ) ) ;
#10372=VECTOR ( 'NONE', #23701, 1000.000000000000114 ) ;
#10441=ORIENTED_EDGE ( 'NONE', *, *, #9488, .F. ) ;
#10529=( LENGTH_UNIT ( ) NAMED_UNIT ( * ) SI_UNIT ( .MILLI., .METRE. ) );
#10653=EDGE_CURVE ( 'NONE', #34825, #40596, #45953, .T. ) ;
#10725=EDGE_CURVE ( 'NONE', #13821, #34386, #53303, .T. ) ;
#10749=CARTESIAN_POINT ( 'NONE',  ( 18.99979856674334044, 49.77026365512251971, 12.50000000000000000 ) ) ;
#10773=CARTESIAN_POINT ( 'NONE',  ( 3.999798566743338668, 8.867945265733711224, -11.56480034751363917 ) ) ;
#10840=CARTESIAN_POINT ( 'NONE',  ( 17.15973193263811680, -3.000000000000000000, 2.000000000000000000 ) ) ;
#10892=SURFACE_STYLE_FILL_AREA ( #15846 ) ;
#10929=LINE ( 'NONE', #53826, #24659 ) ;
#10968=( NAMED_UNIT ( * ) SI_UNIT ( $, .STERADIAN. ) SOLID_ANGLE_UNIT ( ) );
#11021=CARTESIAN_POINT ( 'NONE',  ( -13.23915246117191025, 52.65078610323165265, -12.50000000000000000 ) ) ;
#11051=ORIENTED_EDGE ( 'NONE', *, *, #17200, .T. ) ;
#11092=STYLED_ITEM ( 'NONE', ( #16051 ), #14785 ) ;
#11115=VERTEX_POINT ( 'NONE', #26390 ) ;
#11154=LINE ( 'NONE', #53400, #9639 ) ;
#11184=DIRECTION ( 'NONE',  ( -0.000000000000000000, 0.000000000000000000, 1.000000000000000000 ) ) ;
#11197=COLOUR_RGB ( '', 0.66274510, 0.83137255, 0.94901961) ;
#11231=CYLINDRICAL_SURFACE ( 'NONE', #53181, 1.999999999999998224 ) ;
#11273=ORIENTED_EDGE ( 'NONE', *, *, #6847, .T. ) ;
#11302=FILL_AREA_STYLE_COLOUR ( '', #33145 ) ;
#11314=( NAMED_UNIT ( * ) PLANE_ANGLE_UNIT ( ) SI_UNIT ( $, .RADIAN. ) );
#11369=ADVANCED_FACE ( 'NONE', ( #2730 ), #50621, .T. ) ;
#11411=DIRECTION ( 'NONE',  ( -0.000000000000000000, -0.000000000000000000, -1.000000000000000000 ) ) ;
#11422=DIRECTION ( 'NONE',  ( -0.000000000000000000, -0.000000000000000000, -1.000000000000000000 ) ) ;
#11472=SURFACE_SIDE_STYLE ('',( #23083 ) ) ;
#11563=STYLED_ITEM ( 'NONE', ( #58295 ), #46620 ) ;
#11572=ORIENTED_EDGE ( 'NONE', *, *, #69568, .T. ) ;
#11609=FILL_AREA_STYLE ('',( #22871 ) ) ;
#11729=LINE ( 'NONE', #60937, #24630 ) ;
#11843=( NAMED_UNIT ( * ) PLANE_ANGLE_UNIT ( ) SI_UNIT ( $, .RADIAN. ) );
#11896=PRESENTATION_STYLE_ASSIGNMENT (( #27701 ) ) ;
#11955=PRESENTATION_STYLE_ASSIGNMENT (( #42983 ) ) ;
#12010=MECHANICAL_DESIGN_GEOMETRIC_PRESENTATION_REPRESENTATION('',(#9772),#37920);
#12057=EDGE_CURVE ( 'NONE', #42596, #53696, #44099, .T. ) ;
#12065=DIRECTION ( 'NONE',  ( -0.07854820085872887825, -0.9914125719358882760, 0.1045528208578022367 ) ) ;
#12081=ORIENTED_EDGE ( 'NONE', *, *, #44051, .F. ) ;
#12175=DIRECTION ( 'NONE',  ( -0.000000000000000000, -0.000000000000000000, -1.000000000000000000 ) ) ;
#12250=DIRECTION ( 'NONE',  ( -0.000000000000000000, -0.000000000000000000, 1.000000000000000000 ) ) ;
#12267=FILL_AREA_STYLE ('',( #61492 ) ) ;
#12310=ORIENTED_EDGE ( 'NONE', *, *, #26432, .T. ) ;
#12339=MECHANICAL_DESIGN_GEOMETRIC_PRESENTATION_REPRESENTATION('',(#33688),#51685);
#12424=VECTOR ( 'NONE', #30826, 1000.000000000000000 ) ;
#12492=MECHANICAL_DESIGN_GEOMETRIC_PRESENTATION_REPRESENTATION('',(#14788),#42895);
#12504=PRESENTATION_STYLE_ASSIGNMENT (( #65983 ) ) ;
#12602=EDGE_CURVE ( 'NONE', #53207, #20985, #30107, .T. ) ;
#12859=( NAMED_UNIT ( * ) SI_UNIT ( $, .STERADIAN. ) SOLID_ANGLE_UNIT ( ) );
#12923=MECHANICAL_DESIGN_GEOMETRIC_PRESENTATION_REPRESENTATION('',(#3931),#47860);
#12985=MECHANICAL_DESIGN_GEOMETRIC_PRESENTATION_REPRESENTATION('',(#64666),#19724);
#13079=DIRECTION ( 'NONE',  ( 1.000000000000000000, 0.000000000000000000, 0.000000000000000000 ) ) ;
#13103=FILL_AREA_STYLE ('',( #18402 ) ) ;
#13196=PLANE ( 'NONE',  #8672 ) ;
#13204=CARTESIAN_POINT ( 'NONE',  ( 0.04677136509298115974, 68.99999999999998579, -2.000000000000000000 ) ) ;
#13253=VECTOR ( 'NONE', #64486, 1000.000000000000000 ) ;
#13315=SURFACE_STYLE_USAGE ( .BOTH. , #24225 ) ;
#13368=LINE ( 'NONE', #8111, #45061 ) ;
#13410=EDGE_CURVE ( 'NONE', #1680, #34386, #63146, .T. ) ;
#13419=CARTESIAN_POINT ( 'NONE',  ( -14.95322863490701870, 69.00000000000000000, 6.349999999999997868 ) ) ;
#13427=EDGE_CURVE ( 'NONE', #6296, #34825, #17129, .T. ) ;
#13428=DIRECTION ( 'NONE',  ( -0.000000000000000000, -0.000000000000000000, -1.000000000000000000 ) ) ;
#13434=ORIENTED_EDGE ( 'NONE', *, *, #43281, .F. ) ;
#13449=MECHANICAL_DESIGN_GEOMETRIC_PRESENTATION_REPRESENTATION('',(#33643),#16852);
#13454=DIRECTION ( 'NONE',  ( -0.9968761159932768567, 0.07898106964430656740, 0.000000000000000000 ) ) ;
#13468=ORIENTED_EDGE ( 'NONE', *, *, #47772, .F. ) ;
#13497=EDGE_CURVE ( 'NONE', #22057, #59357, #66835, .T. ) ;
#13616=ADVANCED_FACE ( 'NONE', ( #37281 ), #42549, .T. ) ;
#13781=( LENGTH_UNIT ( ) NAMED_UNIT ( * ) SI_UNIT ( .MILLI., .METRE. ) );
#13782=VECTOR ( 'NONE', #56925, 1000.000000000000000 ) ;
#13793=( GEOMETRIC_REPRESENTATION_CONTEXT ( 3 ) GLOBAL_UNCERTAINTY_ASSIGNED_CONTEXT ( ( #63808 ) ) GLOBAL_UNIT_ASSIGNED_CONTEXT ( ( #59382, #54466, #27713 ) ) REPRESENTATION_CONTEXT ( 'NONE', 'WORKASPACE' ) );
#13821=VERTEX_POINT ( 'NONE', #16840 ) ;
#13845=CARTESIAN_POINT ( 'NONE',  ( -20.29261984882471381, 1.607755262496696869, -6.349999999999987210 ) ) ;
#13865=EDGE_CURVE ( 'NONE', #29661, #51672, #2664, .T. ) ;
#13902=( GEOMETRIC_REPRESENTATION_CONTEXT ( 3 ) GLOBAL_UNCERTAINTY_ASSIGNED_CONTEXT ( ( #25070 ) ) GLOBAL_UNIT_ASSIGNED_CONTEXT ( ( #10529, #54455, #42926 ) ) REPRESENTATION_CONTEXT ( 'NONE', 'WORKASPACE' ) );
#13917=DIRECTION ( 'NONE',  ( -1.000000000000000000, 0.000000000000000000, 0.000000000000000000 ) ) ;
#13933=CARTESIAN_POINT ( 'NONE',  ( 1.804495846578303864, 51.08602766979955589, -7.112547338523483198 ) ) ;
#13953=DIRECTION ( 'NONE',  ( 0.000000000000000000, 0.000000000000000000, 1.000000000000000000 ) ) ;
#13967=SURFACE_STYLE_FILL_AREA ( #51262 ) ;
#14050=CARTESIAN_POINT ( 'NONE',  ( 7.227466682572271317, 6.938893903907228378E-15, -12.50000000000000000 ) ) ;
#14142=ORIENTED_EDGE ( 'NONE', *, *, #33871, .F. ) ;
#14207=ORIENTED_EDGE ( 'NONE', *, *, #7292, .T. ) ;
#14396=LINE ( 'NONE', #14772, #2174 ) ;
#14460=CARTESIAN_POINT ( 'NONE',  ( 0.000000000000000000, 8.270287287112621792E-15, 12.50000000000000000 ) ) ;
#14561=ORIENTED_EDGE ( 'NONE', *, *, #3890, .F. ) ;
#14581=CARTESIAN_POINT ( 'NONE',  ( 3.999798566743339556, 8.867945265733707672, 2.000000000000000000 ) ) ;
#14596=FILL_AREA_STYLE_COLOUR ( '', #54056 ) ;
#14614=FILL_AREA_STYLE ('',( #62447 ) ) ;
#14659=LINE ( 'NONE', #56876, #26397 ) ;
#14680=PRODUCT_DEFINITION_FORMATION_WITH_SPECIFIED_SOURCE ( 'ANY', '', #54094, .NOT_KNOWN. ) ;
#14726=SURFACE_STYLE_FILL_AREA ( #36569 ) ;
#14769=MECHANICAL_DESIGN_GEOMETRIC_PRESENTATION_REPRESENTATION('',(#3452),#20370);
#14772=CARTESIAN_POINT ( 'NONE',  ( 3.999798566743339556, 49.09558629977726696, -2.000000000000000000 ) ) ;
#14785=ADVANCED_FACE ( 'NONE', ( #27229 ), #47754, .F. ) ;
#14788=STYLED_ITEM ( 'NONE', ( #8957 ), #17106 ) ;
#14893=ORIENTED_EDGE ( 'NONE', *, *, #40760, .T. ) ;
#14938=LINE ( 'NONE', #48016, #18543 ) ;
#14956=SURFACE_STYLE_USAGE ( .BOTH. , #56447 ) ;
#15168=PRESENTATION_STYLE_ASSIGNMENT (( #4909 ) ) ;
#15173=ADVANCED_FACE ( 'NONE', ( #39861, #55294 ), #7115, .F. ) ;
#15194=STYLED_ITEM ( 'NONE', ( #62060 ), #38719 ) ;
#15264=EDGE_LOOP ( 'NONE', ( #29735, #27497, #8046, #33633, #22213 ) ) ;
#15345=DIRECTION ( 'NONE',  ( -0.3403530053317448401, 0.9351121967924955758, 0.09861547125863370789 ) ) ;
#15429=LINE ( 'NONE', #27305, #64493 ) ;
#15435=( NAMED_UNIT ( * ) SI_UNIT ( $, .STERADIAN. ) SOLID_ANGLE_UNIT ( ) );
#15523=ADVANCED_FACE ( 'NONE', ( #28102 ), #65062, .F. ) ;
#15532=EDGE_LOOP ( 'NONE', ( #39311, #61967, #24964, #59818 ) ) ;
#15617=MECHANICAL_DESIGN_GEOMETRIC_PRESENTATION_REPRESENTATION('',(#20038),#21148);
#15623=( NAMED_UNIT ( * ) SI_UNIT ( $, .STERADIAN. ) SOLID_ANGLE_UNIT ( ) );
#15655=FILL_AREA_STYLE_COLOUR ( '', #62283 ) ;
#15691=EDGE_CURVE ( 'NONE', #2615, #53207, #41672, .T. ) ;
#15712=UNCERTAINTY_MEASURE_WITH_UNIT (LENGTH_MEASURE( 1.000000000000000082E-05 ), #60246, 'distance_accuracy_value', 'NONE');
#15750=ORIENTED_EDGE ( 'NONE', *, *, #18874, .T. ) ;
#15774=FACE_OUTER_BOUND ( 'NONE', #24902, .T. ) ;
#15846=FILL_AREA_STYLE ('',( #26692 ) ) ;
#15912=COLOUR_RGB ( '', 0.08235294, 0.09019608, 0.10196078) ;
#15922=CARTESIAN_POINT ( 'NONE',  ( 0.04677136509298115974, 68.99999999999998579, 2.000000000000000000 ) ) ;
#15929=VECTOR ( 'NONE', #57196, 1000.000000000000000 ) ;
#16051=PRESENTATION_STYLE_ASSIGNMENT (( #43152 ) ) ;
#16060=ORIENTED_EDGE ( 'NONE', *, *, #16159, .F. ) ;
#16148=( GEOMETRIC_REPRESENTATION_CONTEXT ( 3 ) GLOBAL_UNCERTAINTY_ASSIGNED_CONTEXT ( ( #18748 ) ) GLOBAL_UNIT_ASSIGNED_CONTEXT ( ( #40131, #8087, #33771 ) ) REPRESENTATION_CONTEXT ( 'NONE', 'WORKASPACE' ) );
#16159=EDGE_CURVE ( 'NONE', #29580, #23615, #30267, .T. ) ;
#16174=STYLED_ITEM ( 'NONE', ( #50406 ), #2318 ) ;
#16279=PLANE ( 'NONE',  #59036 ) ;
#16322=EDGE_CURVE ( 'NONE', #34272, #25644, #5991, .T. ) ;
#16329=SURFACE_STYLE_USAGE ( .BOTH. , #32443 ) ;
#16363=PRESENTATION_STYLE_ASSIGNMENT (( #26175 ) ) ;
#16391=LINE ( 'NONE', #48065, #23475 ) ;
#16395=COLOUR_RGB ( '', 0.40784314, 0.44705882, 0.49803922) ;
#16435=LINE ( 'NONE', #4788, #60633 ) ;
#16547=FACE_OUTER_BOUND ( 'NONE', #50064, .T. ) ;
#16591=DIRECTION ( 'NONE',  ( -0.3420201433256663814, 0.9396926207859092051, 0.000000000000000000 ) ) ;
#16621=CARTESIAN_POINT ( 'NONE',  ( -17.41962728626436530, -0.1139526552317604857, -12.50000000000000000 ) ) ;
#16675=ORIENTED_EDGE ( 'NONE', *, *, #58951, .F. ) ;
#16678=ORIENTED_EDGE ( 'NONE', *, *, #25562, .F. ) ;
#16680=CARTESIAN_POINT ( 'NONE',  ( 17.15973193263811680, -3.000000000000000000, 2.000000000000000000 ) ) ;
#16775=ORIENTED_EDGE ( 'NONE', *, *, #33043, .F. ) ;
#16807=SURFACE_STYLE_USAGE ( .BOTH. , #43903 ) ;
#16840=CARTESIAN_POINT ( 'NONE',  ( 20.42000000000000526, 0.000000000000000000, 12.50000000000000000 ) ) ;
#16852=( GEOMETRIC_REPRESENTATION_CONTEXT ( 3 ) GLOBAL_UNCERTAINTY_ASSIGNED_CONTEXT ( ( #27042 ) ) GLOBAL_UNIT_ASSIGNED_CONTEXT ( ( #23627, #2830, #25022 ) ) REPRESENTATION_CONTEXT ( 'NONE', 'WORKASPACE' ) );
#16858=DIRECTION ( 'NONE',  ( 1.000000000000000000, 0.000000000000000000, 0.000000000000000000 ) ) ;
#16896=CARTESIAN_POINT ( 'NONE',  ( 6.999798566743339556, 49.77026365512251971, -7.251305755767528005 ) ) ;
#16916=FILL_AREA_STYLE_COLOUR ( '', #53918 ) ;
#16921=DIRECTION ( 'NONE',  ( -1.068252564556022042E-16, 0.9944852160011111719, 0.1048768571002353378 ) ) ;
#17002=CARTESIAN_POINT ( 'NONE',  ( 6.999798566743339556, 49.77026365512251971, 7.251305755767526229 ) ) ;
#17106=ADVANCED_FACE ( 'NONE', ( #29717 ), #8272, .F. ) ;
#17129=CIRCLE ( 'NONE', #54142, 17.42000000000001236 ) ;
#17151=COLOUR_RGB ( '', 0.08235294, 0.09019608, 0.10196078) ;
#17157=PRESENTATION_STYLE_ASSIGNMENT (( #16807 ) ) ;
#17166=DIRECTION ( 'NONE',  ( -0.000000000000000000, -0.000000000000000000, 1.000000000000000000 ) ) ;
#17200=EDGE_CURVE ( 'NONE', #18031, #443, #62744, .T. ) ;
#17224=ORIENTED_EDGE ( 'NONE', *, *, #51949, .F. ) ;
#17244=( LENGTH_UNIT ( ) NAMED_UNIT ( * ) SI_UNIT ( .MILLI., .METRE. ) );
#17267=CARTESIAN_POINT ( 'NONE',  ( -17.41059898028469277, 6.938893903907228378E-15, -12.50000000000000000 ) ) ;
#17388=( LENGTH_UNIT ( ) NAMED_UNIT ( * ) SI_UNIT ( .MILLI., .METRE. ) );
#17477=( NAMED_UNIT ( * ) PLANE_ANGLE_UNIT ( ) SI_UNIT ( $, .RADIAN. ) );
#17501=FILL_AREA_STYLE ('',( #54054 ) ) ;
#17503=DIRECTION ( 'NONE',  ( -0.07898106964430656740, -0.9968761159932768567, -0.000000000000000000 ) ) ;
#17567=EDGE_LOOP ( 'NONE', ( #55077, #65221, #39828, #31302 ) ) ;
#17608=EDGE_CURVE ( 'NONE', #2615, #63718, #25979, .T. ) ;
#17643=ORIENTED_EDGE ( 'NONE', *, *, #53084, .T. ) ;
#17646=ORIENTED_EDGE ( 'NONE', *, *, #58530, .T. ) ;
#17724=VERTEX_POINT ( 'NONE', #17267 ) ;
#17799=CARTESIAN_POINT ( 'NONE',  ( 17.15973193263811680, -3.000000000000000000, -12.50000000000000000 ) ) ;
#17810=ORIENTED_EDGE ( 'NONE', *, *, #12602, .T. ) ;
#17824=DIRECTION ( 'NONE',  ( 0.3420201433256660484, -0.9396926207859094271, 0.000000000000000000 ) ) ;
#18011=SURFACE_SIDE_STYLE ('',( #44788 ) ) ;
#18023=( NAMED_UNIT ( * ) PLANE_ANGLE_UNIT ( ) SI_UNIT ( $, .RADIAN. ) );
#18031=VERTEX_POINT ( 'NONE', #53703 ) ;
#18066=EDGE_LOOP ( 'NONE', ( #18567, #68152, #62808, #40468 ) ) ;
#18084=CARTESIAN_POINT ( 'NONE',  ( 0.04677136509298115974, 68.99999999999998579, 6.349999999999997868 ) ) ;
#18331=CIRCLE ( 'NONE', #60984, 17.42000000000001236 ) ;
#18339=CARTESIAN_POINT ( 'NONE',  ( 3.999798566743338668, 49.09558629977726696, 7.322456175549363344 ) ) ;
#18386=STYLED_ITEM ( 'NONE', ( #11896 ), #30884 ) ;
#18402=FILL_AREA_STYLE_COLOUR ( '', #34117 ) ;
#18493=FILL_AREA_STYLE ('',( #14596 ) ) ;
#18511=( GEOMETRIC_REPRESENTATION_CONTEXT ( 3 ) GLOBAL_UNCERTAINTY_ASSIGNED_CONTEXT ( ( #8125 ) ) GLOBAL_UNIT_ASSIGNED_CONTEXT ( ( #40651, #29726, #68399 ) ) REPRESENTATION_CONTEXT ( 'NONE', 'WORKASPACE' ) );
#18543=VECTOR ( 'NONE', #25459, 1000.000000000000000 ) ;
#18565=CARTESIAN_POINT ( 'NONE',  ( 1.804495846578303864, 51.08602766979955589, 7.112547338523483198 ) ) ;
#18567=ORIENTED_EDGE ( 'NONE', *, *, #13497, .T. ) ;
#18600=DIRECTION ( 'NONE',  ( -0.07898106964430649801, -0.9968761159932768567, 0.000000000000000000 ) ) ;
#18651=STYLED_ITEM ( 'NONE', ( #15168 ), #662 ) ;
#18730=VERTEX_POINT ( 'NONE', #947 ) ;
#18748=UNCERTAINTY_MEASURE_WITH_UNIT (LENGTH_MEASURE( 1.000000000000000082E-05 ), #40131, 'distance_accuracy_value', 'NONE');
#18824=FILL_AREA_STYLE_COLOUR ( '', #7504 ) ;
#18859=DIRECTION ( 'NONE',  ( 1.000000000000000000, 0.000000000000000000, 0.000000000000000000 ) ) ;
#18874=EDGE_CURVE ( 'NONE', #23615, #34272, #7367, .T. ) ;
#18907=CARTESIAN_POINT ( 'NONE',  ( -20.29261984882471381, 1.607755262496699533, 12.50000000000000000 ) ) ;
#18981=SURFACE_SIDE_STYLE ('',( #8800 ) ) ;
#19001=CARTESIAN_POINT ( 'NONE',  ( 3.999798566743339556, 49.09558629977726696, 2.000000000000000000 ) ) ;
#19005=ADVANCED_FACE ( 'NONE', ( #15774 ), #37254, .F. ) ;
#19032=STYLED_ITEM ( 'NONE', ( #34337 ), #1136 ) ;
#19175=ORIENTED_EDGE ( 'NONE', *, *, #22794, .T. ) ;
#19252=DIRECTION ( 'NONE',  ( -0.07898106964430656740, -0.9968761159932768567, 0.000000000000000000 ) ) ;
#19258=( NAMED_UNIT ( * ) SI_UNIT ( $, .STERADIAN. ) SOLID_ANGLE_UNIT ( ) );
#19278=CARTESIAN_POINT ( 'NONE',  ( 0.000000000000000000, 0.000000000000000000, 12.50000000000000000 ) ) ;
#19383=( GEOMETRIC_REPRESENTATION_CONTEXT ( 3 ) GLOBAL_UNCERTAINTY_ASSIGNED_CONTEXT ( ( #56719 ) ) GLOBAL_UNIT_ASSIGNED_CONTEXT ( ( #57986, #3771, #15435 ) ) REPRESENTATION_CONTEXT ( 'NONE', 'WORKASPACE' ) );
#19434=DIRECTION ( 'NONE',  ( -0.000000000000000000, -0.000000000000000000, -1.000000000000000000 ) ) ;
#19474=AXIS2_PLACEMENT_3D ( 'NONE', #23232, #60842, #66121 ) ;
#19515=COLOUR_RGB ( '', 0.66274510, 0.83137255, 0.94901961) ;
#19530=CARTESIAN_POINT ( 'NONE',  ( 0.000000000000000000, 0.000000000000000000, -2.000000000000000000 ) ) ;
#19604=EDGE_CURVE ( 'NONE', #59357, #69289, #44531, .T. ) ;
#19613=LINE ( 'NONE', #41111, #55315 ) ;
#19724=( GEOMETRIC_REPRESENTATION_CONTEXT ( 3 ) GLOBAL_UNCERTAINTY_ASSIGNED_CONTEXT ( ( #46087 ) ) GLOBAL_UNIT_ASSIGNED_CONTEXT ( ( #61542, #9164, #3111 ) ) REPRESENTATION_CONTEXT ( 'NONE', 'WORKASPACE' ) );
#19801=ORIENTED_EDGE ( 'NONE', *, *, #13865, .T. ) ;
#19956=( NAMED_UNIT ( * ) PLANE_ANGLE_UNIT ( ) SI_UNIT ( $, .RADIAN. ) );
#19974=DIRECTION ( 'NONE',  ( 0.000000000000000000, -0.1048768571002353378, -0.9944852160011111719 ) ) ;
#20038=STYLED_ITEM ( 'NONE', ( #34774 ), #68155 ) ;
#20050=UNCERTAINTY_MEASURE_WITH_UNIT (LENGTH_MEASURE( 1.000000000000000082E-05 ), #46675, 'distance_accuracy_value', 'NONE');
#20142=CARTESIAN_POINT ( 'NONE',  ( 3.999798566743339556, 8.867945265733707672, -2.000000000000000000 ) ) ;
#20193=DIRECTION ( 'NONE',  ( -0.000000000000000000, -0.000000000000000000, -1.000000000000000000 ) ) ;
#20274=LINE ( 'NONE', #56520, #12424 ) ;
#20307=AXIS2_PLACEMENT_3D ( 'NONE', #63277, #58682, #216 ) ;
#20308=( NAMED_UNIT ( * ) SI_UNIT ( $, .STERADIAN. ) SOLID_ANGLE_UNIT ( ) );
#20370=( GEOMETRIC_REPRESENTATION_CONTEXT ( 3 ) GLOBAL_UNCERTAINTY_ASSIGNED_CONTEXT ( ( #8809 ) ) GLOBAL_UNIT_ASSIGNED_CONTEXT ( ( #68078, #3650, #7921 ) ) REPRESENTATION_CONTEXT ( 'NONE', 'WORKASPACE' ) );
#20380=EDGE_LOOP ( 'NONE', ( #4987, #60085, #1666, #43553 ) ) ;
#20387=PRESENTATION_STYLE_ASSIGNMENT (( #40840 ) ) ;
#20536=STYLED_ITEM ( 'NONE', ( #8645 ), #7231 ) ;
#20565=ORIENTED_EDGE ( 'NONE', *, *, #37727, .T. ) ;
#20584=DIRECTION ( 'NONE',  ( -0.000000000000000000, -0.000000000000000000, -1.000000000000000000 ) ) ;
#20620=VECTOR ( 'NONE', #31784, 1000.000000000000000 ) ;
#20690=EDGE_LOOP ( 'NONE', ( #45694, #2892, #42647, #27887, #24871, #34820, #56678, #45780 ) ) ;
#20883=CARTESIAN_POINT ( 'NONE',  ( 17.15973193263811680, -3.000000000000000000, 2.000000000000000000 ) ) ;
#20952=PRODUCT_DEFINITION_SHAPE ( 'NONE', 'NONE',  #7683 ) ;
#20956=SURFACE_STYLE_FILL_AREA ( #48077 ) ;
#20985=VERTEX_POINT ( 'NONE', #57307 ) ;
#21011=FILL_AREA_STYLE ('',( #9782 ) ) ;
#21051=VECTOR ( 'NONE', #7445, 1000.000000000000000 ) ;
#21115=ORIENTED_EDGE ( 'NONE', *, *, #55617, .T. ) ;
#21148=( GEOMETRIC_REPRESENTATION_CONTEXT ( 3 ) GLOBAL_UNCERTAINTY_ASSIGNED_CONTEXT ( ( #58601 ) ) GLOBAL_UNIT_ASSIGNED_CONTEXT ( ( #50971, #55185, #6645 ) ) REPRESENTATION_CONTEXT ( 'NONE', 'WORKASPACE' ) );
#21249=VECTOR ( 'NONE', #4310, 1000.000000000000000 ) ;
#21292=UNCERTAINTY_MEASURE_WITH_UNIT (LENGTH_MEASURE( 1.000000000000000082E-05 ), #67821, 'distance_accuracy_value', 'NONE');
#21305=DIRECTION ( 'NONE',  ( -0.3420201433256663814, 0.9396926207859092051, -0.000000000000000000 ) ) ;
#21386=( NAMED_UNIT ( * ) SI_UNIT ( $, .STERADIAN. ) SOLID_ANGLE_UNIT ( ) );
#21414=ORIENTED_EDGE ( 'NONE', *, *, #2164, .T. ) ;
#21434=DIRECTION ( 'NONE',  ( 1.000000000000000000, 0.000000000000000000, 0.000000000000000000 ) ) ;
#21445=UNCERTAINTY_MEASURE_WITH_UNIT (LENGTH_MEASURE( 1.000000000000000082E-05 ), #59607, 'distance_accuracy_value', 'NONE');
#21446=COLOUR_RGB ( '', 0.31764706, 0.68627451, 0.89019608) ;
#21474=SURFACE_STYLE_FILL_AREA ( #11609 ) ;
#21493=AXIS2_PLACEMENT_3D ( 'NONE', #24417, #67013, #39612 ) ;
#21661=MECHANICAL_DESIGN_GEOMETRIC_PRESENTATION_REPRESENTATION('',(#11563),#25031);
#21711=APPLICATION_CONTEXT ( 'automotive_design' ) ;
#21731=AXIS2_PLACEMENT_3D ( 'NONE', #18907, #24889, #18600 ) ;
#21795=SURFACE_STYLE_FILL_AREA ( #31642 ) ;
#21827=EDGE_LOOP ( 'NONE', ( #7406, #24529, #43218, #68516, #10196, #54492, #62263, #36041 ) ) ;
#21841=CARTESIAN_POINT ( 'NONE',  ( 3.999798566743339556, 8.867945265733707672, -2.000000000000000000 ) ) ;
#21889=AXIS2_PLACEMENT_3D ( 'NONE', #57860, #20193, #52588 ) ;
#21935=VERTEX_POINT ( 'NONE', #29894 ) ;
#21942=LINE ( 'NONE', #4706, #48734 ) ;
#21960=ORIENTED_EDGE ( 'NONE', *, *, #33208, .T. ) ;
#21965=VECTOR ( 'NONE', #47768, 1000.000000000000114 ) ;
#22057=VERTEX_POINT ( 'NONE', #60411 ) ;
#22126=SURFACE_SIDE_STYLE ('',( #28765 ) ) ;
#22137=( NAMED_UNIT ( * ) PLANE_ANGLE_UNIT ( ) SI_UNIT ( $, .RADIAN. ) );
#22139=ORIENTED_EDGE ( 'NONE', *, *, #58792, .T. ) ;
#22181=DIRECTION ( 'NONE',  ( -0.000000000000000000, -0.000000000000000000, 1.000000000000000000 ) ) ;
#22182=UNCERTAINTY_MEASURE_WITH_UNIT (LENGTH_MEASURE( 1.000000000000000082E-05 ), #62178, 'distance_accuracy_value', 'NONE');
#22213=ORIENTED_EDGE ( 'NONE', *, *, #33745, .F. ) ;
#22247=VECTOR ( 'NONE', #8850, 1000.000000000000000 ) ;
#22401=AXIS2_PLACEMENT_3D ( 'NONE', #47227, #8171, #24658 ) ;
#22471=DIRECTION ( 'NONE',  ( -0.000000000000000000, -0.000000000000000000, -1.000000000000000000 ) ) ;
#22485=SURFACE_STYLE_FILL_AREA ( #43635 ) ;
#22637=( NAMED_UNIT ( * ) PLANE_ANGLE_UNIT ( ) SI_UNIT ( $, .RADIAN. ) );
#22731=( LENGTH_UNIT ( ) NAMED_UNIT ( * ) SI_UNIT ( .MILLI., .METRE. ) );
#22742=( NAMED_UNIT ( * ) PLANE_ANGLE_UNIT ( ) SI_UNIT ( $, .RADIAN. ) );
#22793=EDGE_LOOP ( 'NONE', ( #21414, #57067, #12310, #50713 ) ) ;
#22794=EDGE_CURVE ( 'NONE', #42291, #2399, #62261, .T. ) ;
#22811=FACE_OUTER_BOUND ( 'NONE', #36582, .T. ) ;
#22827=VERTEX_POINT ( 'NONE', #251 ) ;
#22850=STYLED_ITEM ( 'NONE', ( #5945 ), #55422 ) ;
#22868=CIRCLE ( 'NONE', #49826, 1.999999999999998224 ) ;
#22871=FILL_AREA_STYLE_COLOUR ( '', #61158 ) ;
#22887=AXIS2_PLACEMENT_3D ( 'NONE', #39532, #13454, #24692 ) ;
#22903=( GEOMETRIC_REPRESENTATION_CONTEXT ( 3 ) GLOBAL_UNCERTAINTY_ASSIGNED_CONTEXT ( ( #22182 ) ) GLOBAL_UNIT_ASSIGNED_CONTEXT ( ( #62178, #19956, #19258 ) ) REPRESENTATION_CONTEXT ( 'NONE', 'WORKASPACE' ) );
#22941=DIRECTION ( 'NONE',  ( -0.000000000000000000, -0.000000000000000000, -1.000000000000000000 ) ) ;
#22965=( NAMED_UNIT ( * ) PLANE_ANGLE_UNIT ( ) SI_UNIT ( $, .RADIAN. ) );
#22970=ADVANCED_FACE ( 'NONE', ( #6979 ), #32663, .T. ) ;
#22974=EDGE_LOOP ( 'NONE', ( #22139, #45791, #63371, #9153 ) ) ;
#23083=SURFACE_STYLE_FILL_AREA ( #65974 ) ;
#23141=STYLED_ITEM ( 'NONE', ( #5585 ), #58288 ) ;
#23186=( NAMED_UNIT ( * ) SI_UNIT ( $, .STERADIAN. ) SOLID_ANGLE_UNIT ( ) );
#23188=CARTESIAN_POINT ( 'NONE',  ( -14.95322863490701870, 69.00000000000000000, -6.349999999999994316 ) ) ;
#23232=CARTESIAN_POINT ( 'NONE',  ( 1.999798566743339334, 49.09558629977726696, -2.000000000000000000 ) ) ;
#23260=CARTESIAN_POINT ( 'NONE',  ( 1.804495846578303864, 51.08602766979955589, 7.112547338523483198 ) ) ;
#23277=( BOUNDED_CURVE ( )  B_SPLINE_CURVE ( 3, ( #4731, #68418, #41714, #4356 ),
 .UNSPECIFIED., .F., .F. ) 
 B_SPLINE_CURVE_WITH_KNOTS ( ( 4, 4 ),
 ( 1.649859741910239874, 3.741551587622924835 ),
 .UNSPECIFIED. ) 
 CURVE ( )  GEOMETRIC_REPRESENTATION_ITEM ( )  RATIONAL_B_SPLINE_CURVE ( ( 1.000000000000000000, 0.6674467249320013007, 0.6674467249320013007, 1.000000000000000000 ) ) 
 REPRESENTATION_ITEM ( '' )  );
#23475=VECTOR ( 'NONE', #11411, 1000.000000000000000 ) ;
#23524=CARTESIAN_POINT ( 'NONE',  ( -10.11618306975752368, 54.14354156754873060, 6.790106699912857202 ) ) ;
#23606=AXIS2_PLACEMENT_3D ( 'NONE', #67866, #57289, #46803 ) ;
#23615=VERTEX_POINT ( 'NONE', #42775 ) ;
#23627=( LENGTH_UNIT ( ) NAMED_UNIT ( * ) SI_UNIT ( .MILLI., .METRE. ) );
#23658=EDGE_CURVE ( 'NONE', #36574, #2399, #23277, .T. ) ;
#23673=UNCERTAINTY_MEASURE_WITH_UNIT (LENGTH_MEASURE( 1.000000000000000082E-05 ), #33078, 'distance_accuracy_value', 'NONE');
#23701=DIRECTION ( 'NONE',  ( 0.07898106964430649801, 0.9968761159932768567, -1.346643164337371088E-16 ) ) ;
#23783=CARTESIAN_POINT ( 'NONE',  ( -10.11618306975752368, 54.14354156754873060, -6.790106699912857202 ) ) ;
#23928=COLOUR_RGB ( '', 0.40784314, 0.44705882, 0.49803922) ;
#23933=CARTESIAN_POINT ( 'NONE',  ( -10.11618306975752368, 54.14354156754873060, 2.000000000000000000 ) ) ;
#23960=CARTESIAN_POINT ( 'NONE',  ( 3.046771365092978190, 72.00000000000001421, 12.50000000000000000 ) ) ;
#24010=ORIENTED_EDGE ( 'NONE', *, *, #64385, .F. ) ;
#24058=( GEOMETRIC_REPRESENTATION_CONTEXT ( 3 ) GLOBAL_UNCERTAINTY_ASSIGNED_CONTEXT ( ( #20050 ) ) GLOBAL_UNIT_ASSIGNED_CONTEXT ( ( #46675, #25496, #62084 ) ) REPRESENTATION_CONTEXT ( 'NONE', 'WORKASPACE' ) );
#24086=CARTESIAN_POINT ( 'NONE',  ( -1.953228634907021810, 72.00000000000001421, 6.349999999999997868 ) ) ;
#24089=SURFACE_STYLE_FILL_AREA ( #8617 ) ;
#24114=STYLED_ITEM ( 'NONE', ( #16363 ), #62317 ) ;
#24130=CARTESIAN_POINT ( 'NONE',  ( -13.23915246117191025, 52.65078610323165265, -6.947530358905292580 ) ) ;
#24170=ORIENTED_EDGE ( 'NONE', *, *, #37794, .F. ) ;
#24211=LINE ( 'NONE', #66799, #13782 ) ;
#24222=FILL_AREA_STYLE ('',( #35131 ) ) ;
#24225=SURFACE_SIDE_STYLE ('',( #33734 ) ) ;
#24295=LINE ( 'NONE', #19001, #21051 ) ;
#24333=CARTESIAN_POINT ( 'NONE',  ( -20.42000000000000881, -1.426810058990923835E-13, 12.50000000000000000 ) ) ;
#24417=CARTESIAN_POINT ( 'NONE',  ( 3.999798566743339556, 49.09558629977726696, 2.000000000000000000 ) ) ;
#24490=CARTESIAN_POINT ( 'NONE',  ( 1.804495846578303864, 51.08602766979955589, 2.000000000000000000 ) ) ;
#24493=SURFACE_STYLE_USAGE ( .BOTH. , #3007 ) ;
#24529=ORIENTED_EDGE ( 'NONE', *, *, #13427, .T. ) ;
#24549=CARTESIAN_POINT ( 'NONE',  ( -2.448909842207114274, 50.66868219381804295, 7.156559940361793437 ) ) ;
#24604=CARTESIAN_POINT ( 'NONE',  ( 17.15973193263811680, -3.000000000000000000, 2.000000000000000000 ) ) ;
#24610=COLOUR_RGB ( '', 0.08235294, 0.09019608, 0.10196078) ;
#24630=VECTOR ( 'NONE', #12065, 1000.000000000000227 ) ;
#24654=FILL_AREA_STYLE_COLOUR ( '', #19515 ) ;
#24658=DIRECTION ( 'NONE',  ( 1.000000000000000000, 0.000000000000000000, 0.000000000000000000 ) ) ;
#24659=VECTOR ( 'NONE', #16921, 1000.000000000000114 ) ;
#24689=VECTOR ( 'NONE', #16591, 1000.000000000000227 ) ;
#24692=DIRECTION ( 'NONE',  ( -0.07898106964430656740, -0.9968761159932768567, 0.000000000000000000 ) ) ;
#24749=CIRCLE ( 'NONE', #41625, 17.42000000000001236 ) ;
#24759=SURFACE_STYLE_USAGE ( .BOTH. , #29350 ) ;
#24849=AXIS2_PLACEMENT_3D ( 'NONE', #23960, #22941, #44438 ) ;
#24871=ORIENTED_EDGE ( 'NONE', *, *, #67748, .F. ) ;
#24886=DIRECTION ( 'NONE',  ( 1.074176415464006764E-16, -1.000000000000000000, 0.000000000000000000 ) ) ;
#24889=DIRECTION ( 'NONE',  ( -0.9968761159932768567, 0.07898106964430649801, 0.000000000000000000 ) ) ;
#24902=EDGE_LOOP ( 'NONE', ( #40072, #69116, #55152, #68019 ) ) ;
#24908=ORIENTED_EDGE ( 'NONE', *, *, #33043, .T. ) ;
#24909=DIRECTION ( 'NONE',  ( -0.000000000000000000, 0.000000000000000000, 1.000000000000000000 ) ) ;
#24964=ORIENTED_EDGE ( 'NONE', *, *, #16159, .T. ) ;
#25022=( NAMED_UNIT ( * ) SI_UNIT ( $, .STERADIAN. ) SOLID_ANGLE_UNIT ( ) );
#25031=( GEOMETRIC_REPRESENTATION_CONTEXT ( 3 ) GLOBAL_UNCERTAINTY_ASSIGNED_CONTEXT ( ( #21292 ) ) GLOBAL_UNIT_ASSIGNED_CONTEXT ( ( #67821, #47088, #20308 ) ) REPRESENTATION_CONTEXT ( 'NONE', 'WORKASPACE' ) );
#25070=UNCERTAINTY_MEASURE_WITH_UNIT (LENGTH_MEASURE( 1.000000000000000082E-05 ), #10529, 'distance_accuracy_value', 'NONE');
#25089=ORIENTED_EDGE ( 'NONE', *, *, #2230, .F. ) ;
#25291=FILL_AREA_STYLE_COLOUR ( '', #39427 ) ;
#25459=DIRECTION ( 'NONE',  ( -0.000000000000000000, -0.000000000000000000, -1.000000000000000000 ) ) ;
#25471=MECHANICAL_DESIGN_GEOMETRIC_PRESENTATION_REPRESENTATION('',(#58041),#661);
#25476=ORIENTED_EDGE ( 'NONE', *, *, #45318, .T. ) ;
#25496=( NAMED_UNIT ( * ) PLANE_ANGLE_UNIT ( ) SI_UNIT ( $, .RADIAN. ) );
#25499=CARTESIAN_POINT ( 'NONE',  ( 20.42000000000000526, 0.000000000000000000, 12.50000000000000000 ) ) ;
#25562=EDGE_CURVE ( 'NONE', #31257, #40876, #53042, .T. ) ;
#25563=EDGE_CURVE ( 'NONE', #29661, #4018, #33899, .T. ) ;
#25644=VERTEX_POINT ( 'NONE', #20142 ) ;
#25652=FILL_AREA_STYLE_COLOUR ( '', #16395 ) ;
#25663=CARTESIAN_POINT ( 'NONE',  ( 10.57623092156539535, 58.31681314173471975, 6.349999999999996092 ) ) ;
#25777=COLOUR_RGB ( '', 0.31764706, 0.68627451, 0.89019608) ;
#25947=CARTESIAN_POINT ( 'NONE',  ( -11.24540022918535698, 52.49282396394303873, -2.000000000000000000 ) ) ;
#25979=LINE ( 'NONE', #42559, #59537 ) ;
#26098=CARTESIAN_POINT ( 'NONE',  ( 6.999798566743336004, 53.02677333163759243, 6.907879333238360786 ) ) ;
#26140=LINE ( 'NONE', #20883, #21249 ) ;
#26175=SURFACE_STYLE_USAGE ( .BOTH. , #53943 ) ;
#26224=EDGE_LOOP ( 'NONE', ( #68672, #60280, #16678 ) ) ;
#26275=EDGE_CURVE ( 'NONE', #3117, #36574, #50623, .T. ) ;
#26317=DIRECTION ( 'NONE',  ( 1.000000000000000000, 0.000000000000000000, 0.000000000000000000 ) ) ;
#26364=( LENGTH_UNIT ( ) NAMED_UNIT ( * ) SI_UNIT ( .MILLI., .METRE. ) );
#26390=CARTESIAN_POINT ( 'NONE',  ( 6.999798566743339556, 49.77026365512251971, 7.251305755767526229 ) ) ;
#26397=VECTOR ( 'NONE', #51953, 1000.000000000000000 ) ;
#26409=VERTEX_POINT ( 'NONE', #68537 ) ;
#26413=DIRECTION ( 'NONE',  ( 0.000000000000000000, -1.000000000000000000, 1.156482317317871478E-16 ) ) ;
#26432=EDGE_CURVE ( 'NONE', #46838, #9321, #22868, .T. ) ;
#26434=SURFACE_SIDE_STYLE ('',( #64774 ) ) ;
#26510=DIRECTION ( 'NONE',  ( -0.000000000000000000, -0.000000000000000000, 1.000000000000000000 ) ) ;
#26523=PLANE ( 'NONE',  #31948 ) ;
#26580=CARTESIAN_POINT ( 'NONE',  ( 6.999798566743339556, 49.77026365512251971, -7.251305755767528005 ) ) ;
#26659=CARTESIAN_POINT ( 'NONE',  ( -15.79964225816357626, 58.31681314173472686, -6.349999999999996092 ) ) ;
#26692=FILL_AREA_STYLE_COLOUR ( '', #56830 ) ;
#26698=DIRECTION ( 'NONE',  ( 1.000000000000000000, 0.000000000000000000, 0.000000000000000000 ) ) ;
#26805=PRESENTATION_STYLE_ASSIGNMENT (( #16329 ) ) ;
#26838=( LENGTH_UNIT ( ) NAMED_UNIT ( * ) SI_UNIT ( .MILLI., .METRE. ) );
#26968=COLOUR_RGB ( '', 0.72549020, 0.75294118, 0.79215686) ;
#26991=CARTESIAN_POINT ( 'NONE',  ( 0.000000000000000000, 0.000000000000000000, -12.50000000000000000 ) ) ;
#27042=UNCERTAINTY_MEASURE_WITH_UNIT (LENGTH_MEASURE( 1.000000000000000082E-05 ), #23627, 'distance_accuracy_value', 'NONE');
#27105=LINE ( 'NONE', #38076, #46162 ) ;
#27106=( NAMED_UNIT ( * ) PLANE_ANGLE_UNIT ( ) SI_UNIT ( $, .RADIAN. ) );
#27139=ORIENTED_EDGE ( 'NONE', *, *, #17608, .F. ) ;
#27183=CARTESIAN_POINT ( 'NONE',  ( -17.41962728626436530, -0.1139526552317604857, 2.000000000000000000 ) ) ;
#27192=DIRECTION ( 'NONE',  ( 9.811390859391774840E-17, -1.000000000000000000, 0.000000000000000000 ) ) ;
#27229=FACE_OUTER_BOUND ( 'NONE', #5505, .T. ) ;
#27258=DIRECTION ( 'NONE',  ( 0.000000000000000000, -0.9944852160011111719, -0.1048768571002353378 ) ) ;
#27265=STYLED_ITEM ( 'NONE', ( #67461 ), #55549 ) ;
#27273=PLANE ( 'NONE',  #54040 ) ;
#27305=CARTESIAN_POINT ( 'NONE',  ( -12.94269599874522214, 56.39257344741367461, -6.552927311739624727 ) ) ;
#27306=CARTESIAN_POINT ( 'NONE',  ( 17.15973193263811680, -3.000000000000000000, -2.000000000000000000 ) ) ;
#27320=MANIFOLD_SOLID_BREP ( 'Mirror1', #45260 ) ;
#27357=DIRECTION ( 'NONE',  ( -0.000000000000000000, -0.000000000000000000, 1.000000000000000000 ) ) ;
#27497=ORIENTED_EDGE ( 'NONE', *, *, #66964, .F. ) ;
#27547=FACE_OUTER_BOUND ( 'NONE', #34406, .T. ) ;
#27605=AXIS2_PLACEMENT_3D ( 'NONE', #37325, #58380, #59070 ) ;
#27642=STYLED_ITEM ( 'NONE', ( #17157 ), #64881 ) ;
#27697=FILL_AREA_STYLE_COLOUR ( '', #3876 ) ;
#27701=SURFACE_STYLE_USAGE ( .BOTH. , #6269 ) ;
#27713=( NAMED_UNIT ( * ) SI_UNIT ( $, .STERADIAN. ) SOLID_ANGLE_UNIT ( ) );
#27732=UNCERTAINTY_MEASURE_WITH_UNIT (LENGTH_MEASURE( 1.000000000000000082E-05 ), #31237, 'distance_accuracy_value', 'NONE');
#27757=VECTOR ( 'NONE', #19252, 1000.000000000000114 ) ;
#27783=VECTOR ( 'NONE', #56556, 1000.000000000000000 ) ;
#27804=CARTESIAN_POINT ( 'NONE',  ( 3.999798566743343109, 50.36012635523414360, 7.189099757012595404 ) ) ;
#27835=CIRCLE ( 'NONE', #4235, 5.000000000000004441 ) ;
#27844=CYLINDRICAL_SURFACE ( 'NONE', #68474, 5.000000000000000000 ) ;
#27887=ORIENTED_EDGE ( 'NONE', *, *, #56448, .F. ) ;
#27916=ADVANCED_FACE ( 'NONE', ( #40171 ), #6735, .F. ) ;
#27990=CARTESIAN_POINT ( 'NONE',  ( -13.23915246117191025, 52.65078610323165265, -2.000000000000000000 ) ) ;
#27998=CARTESIAN_POINT ( 'NONE',  ( 1.999798566743339334, 49.09558629977726696, -2.000000000000000000 ) ) ;
#28064=DIRECTION ( 'NONE',  ( 1.000000000000000000, 0.000000000000000000, 0.000000000000000000 ) ) ;
#28102=FACE_OUTER_BOUND ( 'NONE', #41212, .T. ) ;
#28161=FILL_AREA_STYLE ('',( #50705 ) ) ;
#28545=FILL_AREA_STYLE_COLOUR ( '', #11197 ) ;
#28552=PRESENTATION_STYLE_ASSIGNMENT (( #6416 ) ) ;
#28628=DIRECTION ( 'NONE',  ( -0.3420201433256663814, 0.9396926207859092051, -0.000000000000000000 ) ) ;
#28700=CARTESIAN_POINT ( 'NONE',  ( 1.804495846578303864, 51.08602766979955589, -2.000000000000000000 ) ) ;
#28732=MECHANICAL_DESIGN_GEOMETRIC_PRESENTATION_REPRESENTATION('',(#23141),#68087);
#28765=SURFACE_STYLE_FILL_AREA ( #45000 ) ;
#28921=SURFACE_STYLE_FILL_AREA ( #13103 ) ;
#28974=EDGE_CURVE ( 'NONE', #40596, #44849, #4217, .T. ) ;
#28990=PRODUCT_CONTEXT ( 'NONE', #21711, 'mechanical' ) ;
#29012=FACE_OUTER_BOUND ( 'NONE', #66136, .T. ) ;
#29064=CARTESIAN_POINT ( 'NONE',  ( -37.50000000000000000, 58.31681314173471975, -6.349999999999996092 ) ) ;
#29107=SURFACE_STYLE_USAGE ( .BOTH. , #56205 ) ;
#29155=AXIS2_PLACEMENT_3D ( 'NONE', #67594, #67239, #46887 ) ;
#29185=ORIENTED_EDGE ( 'NONE', *, *, #42457, .T. ) ;
#29247=LINE ( 'NONE', #2836, #43856 ) ;
#29350=SURFACE_SIDE_STYLE ('',( #24089 ) ) ;
#29511=EDGE_LOOP ( 'NONE', ( #53368, #12081, #50018, #43569 ) ) ;
#29512=ADVANCED_FACE ( 'NONE', ( #45755 ), #29532, .T. ) ;
#29532=PLANE ( 'NONE',  #19474 ) ;
#29556=DIRECTION ( 'NONE',  ( 0.07854820085872887825, 0.9914125719358882760, 0.1045528208578022367 ) ) ;
#29557=FACE_OUTER_BOUND ( 'NONE', #18066, .T. ) ;
#29580=VERTEX_POINT ( 'NONE', #30206 ) ;
#29661=VERTEX_POINT ( 'NONE', #26659 ) ;
#29678=DIRECTION ( 'NONE',  ( 0.000000000000000000, 1.350863103983176297E-16, -1.000000000000000000 ) ) ;
#29713=PRODUCT_DEFINITION_CONTEXT ( 'detailed design', #67111, 'design' ) ;
#29717=FACE_OUTER_BOUND ( 'NONE', #17567, .T. ) ;
#29726=( NAMED_UNIT ( * ) PLANE_ANGLE_UNIT ( ) SI_UNIT ( $, .RADIAN. ) );
#29735=ORIENTED_EDGE ( 'NONE', *, *, #62754, .T. ) ;
#29798=LINE ( 'NONE', #24490, #30345 ) ;
#29885=FILL_AREA_STYLE_COLOUR ( '', #52040 ) ;
#29894=CARTESIAN_POINT ( 'NONE',  ( 3.999798566743338668, 49.09558629977726696, 7.322456175549363344 ) ) ;
#30003=CARTESIAN_POINT ( 'NONE',  ( 3.046771365092978190, 72.00000000000001421, -6.349999999999997868 ) ) ;
#30061=SURFACE_STYLE_USAGE ( .BOTH. , #62432 ) ;
#30077=DIRECTION ( 'NONE',  ( -0.000000000000000000, -0.000000000000000000, -1.000000000000000000 ) ) ;
#30079=ADVANCED_FACE ( 'NONE', ( #68482 ), #31163, .F. ) ;
#30107=LINE ( 'NONE', #9028, #15929 ) ;
#30156=FILL_AREA_STYLE_COLOUR ( '', #39683 ) ;
#30198=SURFACE_SIDE_STYLE ('',( #4508 ) ) ;
#30206=CARTESIAN_POINT ( 'NONE',  ( -17.41962728626436530, -0.1139526552317604857, -2.000000000000000000 ) ) ;
#30267=CIRCLE ( 'NONE', #22401, 17.42000000000001236 ) ;
#30345=VECTOR ( 'NONE', #46000, 1000.000000000000000 ) ;
#30367=DIRECTION ( 'NONE',  ( -0.000000000000000000, -0.000000000000000000, -1.000000000000000000 ) ) ;
#30373=AXIS2_PLACEMENT_3D ( 'NONE', #62671, #63721, #52513 ) ;
#30407=SURFACE_SIDE_STYLE ('',( #61725 ) ) ;
#30433=STYLED_ITEM ( 'NONE', ( #10161 ), #13616 ) ;
#30579=DIRECTION ( 'NONE',  ( -9.811390859391774840E-17, 1.000000000000000000, 0.000000000000000000 ) ) ;
#30595=ORIENTED_EDGE ( 'NONE', *, *, #46685, .F. ) ;
#30764=( LENGTH_UNIT ( ) NAMED_UNIT ( * ) SI_UNIT ( .MILLI., .METRE. ) );
#30821=STYLED_ITEM ( 'NONE', ( #11955 ), #27320 ) ;
#30826=DIRECTION ( 'NONE',  ( 0.000000000000000000, -0.9944852160011111719, 0.1048768571002353378 ) ) ;
#30829=ORIENTED_EDGE ( 'NONE', *, *, #41274, .F. ) ;
#30884=ADVANCED_FACE ( 'NONE', ( #22811 ), #48192, .F. ) ;
#30890=CARTESIAN_POINT ( 'NONE',  ( -17.41962728626436530, -0.1139526552317604857, 12.50000000000000000 ) ) ;
#30982=CARTESIAN_POINT ( 'NONE',  ( 3.999798566743343109, 50.36012635523414360, -7.189099757012595404 ) ) ;
#31115=DIRECTION ( 'NONE',  ( -1.000000000000000000, -9.811390859391773608E-17, -0.000000000000000000 ) ) ;
#31163=CYLINDRICAL_SURFACE ( 'NONE', #40959, 1.999999999999998224 ) ;
#31183=ADVANCED_FACE ( 'NONE', ( #45498 ), #6485, .T. ) ;
#31237=( LENGTH_UNIT ( ) NAMED_UNIT ( * ) SI_UNIT ( .MILLI., .METRE. ) );
#31241=PLANE ( 'NONE',  #44998 ) ;
#31257=VERTEX_POINT ( 'NONE', #13419 ) ;
#31302=ORIENTED_EDGE ( 'NONE', *, *, #53904, .F. ) ;
#31354=SURFACE_STYLE_USAGE ( .BOTH. , #26434 ) ;
#31421=LINE ( 'NONE', #16680, #20620 ) ;
#31569=CARTESIAN_POINT ( 'NONE',  ( 3.062509476195515228E-31, -2.500728763858896269E-15, 12.50000000000000000 ) ) ;
#31580=ORIENTED_EDGE ( 'NONE', *, *, #45397, .F. ) ;
#31588=STYLED_ITEM ( 'NONE', ( #38803 ), #27916 ) ;
#31597=SHAPE_REPRESENTATION ( '3. Padlock', ( #42840 ), #60796 ) ;
#31642=FILL_AREA_STYLE ('',( #42948 ) ) ;
#31686=VECTOR ( 'NONE', #34085, 1000.000000000000000 ) ;
#31761=AXIS2_PLACEMENT_3D ( 'NONE', #920, #22471, #43967 ) ;
#31764=CARTESIAN_POINT ( 'NONE',  ( 3.046771365092978190, 72.00000000000001421, 12.50000000000000000 ) ) ;
#31784=DIRECTION ( 'NONE',  ( -1.000000000000000000, -9.811390859391773608E-17, 0.000000000000000000 ) ) ;
#31823=ORIENTED_EDGE ( 'NONE', *, *, #6847, .F. ) ;
#31861=MECHANICAL_DESIGN_GEOMETRIC_PRESENTATION_REPRESENTATION('',(#27265),#22903);
#31948=AXIS2_PLACEMENT_3D ( 'NONE', #32157, #27192, #38166 ) ;
#32032=DIRECTION ( 'NONE',  ( 0.000000000000000000, 1.350863103983176297E-16, -1.000000000000000000 ) ) ;
#32072=( NAMED_UNIT ( * ) SI_UNIT ( $, .STERADIAN. ) SOLID_ANGLE_UNIT ( ) );
#32139=EDGE_CURVE ( 'NONE', #33557, #26409, #14659, .T. ) ;
#32157=CARTESIAN_POINT ( 'NONE',  ( 17.15973193263811680, -3.000000000000000000, -2.000000000000000000 ) ) ;
#32387=ORIENTED_EDGE ( 'NONE', *, *, #5211, .F. ) ;
#32423=EDGE_LOOP ( 'NONE', ( #1691, #17224, #29185, #48969, #32387 ) ) ;
#32431=COLOUR_RGB ( '', 0.72549020, 0.75294118, 0.79215686) ;
#32443=SURFACE_SIDE_STYLE ('',( #49346 ) ) ;
#32469=LINE ( 'NONE', #27183, #52736 ) ;
#32589=DIRECTION ( 'NONE',  ( -0.9396926207859094271, -0.3420201433256660484, 0.000000000000000000 ) ) ;
#32663=CYLINDRICAL_SURFACE ( 'NONE', #31761, 20.42000000000000526 ) ;
#32678=FILL_AREA_STYLE_COLOUR ( '', #41966 ) ;
#32681=CARTESIAN_POINT ( 'NONE',  ( 0.000000000000000000, 0.000000000000000000, 12.50000000000000000 ) ) ;
#32693=( GEOMETRIC_REPRESENTATION_CONTEXT ( 3 ) GLOBAL_UNCERTAINTY_ASSIGNED_CONTEXT ( ( #36841 ) ) GLOBAL_UNIT_ASSIGNED_CONTEXT ( ( #49351, #18023, #2111 ) ) REPRESENTATION_CONTEXT ( 'NONE', 'WORKASPACE' ) );
#32944=SURFACE_STYLE_USAGE ( .BOTH. , #11472 ) ;
#33030=FILL_AREA_STYLE_COLOUR ( '', #23928 ) ;
#33043=EDGE_CURVE ( 'NONE', #3437, #1680, #9584, .T. ) ;
#33078=( LENGTH_UNIT ( ) NAMED_UNIT ( * ) SI_UNIT ( .MILLI., .METRE. ) );
#33145=COLOUR_RGB ( '', 0.31764706, 0.68627451, 0.89019608) ;
#33176=FILL_AREA_STYLE ('',( #59891 ) ) ;
#33208=EDGE_CURVE ( 'NONE', #45813, #60757, #29798, .T. ) ;
#33210=CARTESIAN_POINT ( 'NONE',  ( 10.42000000000000348, -1.224646799147353651E-15, -12.50000000000000000 ) ) ;
#33313=CARTESIAN_POINT ( 'NONE',  ( 9.201091548649898755, 3.348923446466848475, 12.50000000000000000 ) ) ;
#33352=ORIENTED_EDGE ( 'NONE', *, *, #15691, .F. ) ;
#33385=ORIENTED_EDGE ( 'NONE', *, *, #44535, .F. ) ;
#33444=ORIENTED_EDGE ( 'NONE', *, *, #45998, .T. ) ;
#33459=CARTESIAN_POINT ( 'NONE',  ( 8.046771365092977746, 72.00000000000001421, 6.349999999999997868 ) ) ;
#33523=CARTESIAN_POINT ( 'NONE',  ( -20.29261984882471381, 1.607755262496700421, 6.349999999999988098 ) ) ;
#33547=MECHANICAL_DESIGN_GEOMETRIC_PRESENTATION_REPRESENTATION('',(#11092),#38119);
#33557=VERTEX_POINT ( 'NONE', #14581 ) ;
#33585=PRESENTATION_STYLE_ASSIGNMENT (( #65595 ) ) ;
#33633=ORIENTED_EDGE ( 'NONE', *, *, #4612, .T. ) ;
#33642=( LENGTH_UNIT ( ) NAMED_UNIT ( * ) SI_UNIT ( .MILLI., .METRE. ) );
#33643=STYLED_ITEM ( 'NONE', ( #55649 ), #15173 ) ;
#33649=CARTESIAN_POINT ( 'NONE',  ( -13.23915246117191025, 52.65078610323165265, -6.947530358905292580 ) ) ;
#33688=STYLED_ITEM ( 'NONE', ( #1341 ), #15523 ) ;
#33734=SURFACE_STYLE_FILL_AREA ( #12267 ) ;
#33745=EDGE_CURVE ( 'NONE', #17724, #6296, #54278, .T. ) ;
#33771=( NAMED_UNIT ( * ) SI_UNIT ( $, .STERADIAN. ) SOLID_ANGLE_UNIT ( ) );
#33871=EDGE_CURVE ( 'NONE', #31257, #8740, #49369, .T. ) ;
#33899=LINE ( 'NONE', #13845, #10372 ) ;
#34020=VECTOR ( 'NONE', #40150, 1000.000000000000000 ) ;
#34075=CARTESIAN_POINT ( 'NONE',  ( -13.23915246117191025, 52.65078610323165265, 6.947530358905294356 ) ) ;
#34080=ORIENTED_EDGE ( 'NONE', *, *, #50753, .T. ) ;
#34085=DIRECTION ( 'NONE',  ( -1.000000000000000000, -9.811390859391773608E-17, -0.000000000000000000 ) ) ;
#34117=COLOUR_RGB ( '', 0.08235294, 0.09019608, 0.10196078) ;
#34157=CARTESIAN_POINT ( 'NONE',  ( 8.319377385370872346, -3.000000000000000888, -12.50000000000000000 ) ) ;
#34181=SURFACE_STYLE_FILL_AREA ( #28161 ) ;
#34272=VERTEX_POINT ( 'NONE', #55228 ) ;
#34324=DIRECTION ( 'NONE',  ( 0.07898106964430656740, 0.9968761159932768567, 0.000000000000000000 ) ) ;
#34337=PRESENTATION_STYLE_ASSIGNMENT (( #56476 ) ) ;
#34365=ORIENTED_EDGE ( 'NONE', *, *, #64011, .F. ) ;
#34386=VERTEX_POINT ( 'NONE', #52068 ) ;
#34391=EDGE_CURVE ( 'NONE', #44875, #53696, #14396, .T. ) ;
#34406=EDGE_LOOP ( 'NONE', ( #67816, #13468, #15750, #66317 ) ) ;
#34437=( NAMED_UNIT ( * ) SI_UNIT ( $, .STERADIAN. ) SOLID_ANGLE_UNIT ( ) );
#34503=CIRCLE ( 'NONE', #57000, 20.42000000000000526 ) ;
#34592=DIRECTION ( 'NONE',  ( 0.000000000000000000, 1.000000000000000000, 1.156482317317871478E-16 ) ) ;
#34651=FILL_AREA_STYLE ('',( #18824 ) ) ;
#34656=( LENGTH_UNIT ( ) NAMED_UNIT ( * ) SI_UNIT ( .MILLI., .METRE. ) );
#34657=CYLINDRICAL_SURFACE ( 'NONE', #8355, 17.99999999999999645 ) ;
#34662=( LENGTH_UNIT ( ) NAMED_UNIT ( * ) SI_UNIT ( .MILLI., .METRE. ) );
#34664=CARTESIAN_POINT ( 'NONE',  ( -2.448909842207114274, 50.66868219381804295, -7.156559940361793437 ) ) ;
#34674=CARTESIAN_POINT ( 'NONE',  ( -11.54296011127659050, 55.11956624581093678, -6.687176662279907369 ) ) ;
#34744=CARTESIAN_POINT ( 'NONE',  ( 6.999798566743339556, 49.77026365512251971, 12.50000000000000000 ) ) ;
#34754=( GEOMETRIC_REPRESENTATION_CONTEXT ( 3 ) GLOBAL_UNCERTAINTY_ASSIGNED_CONTEXT ( ( #4449 ) ) GLOBAL_UNIT_ASSIGNED_CONTEXT ( ( #34662, #51214, #35023 ) ) REPRESENTATION_CONTEXT ( 'NONE', 'WORKASPACE' ) );
#34774=PRESENTATION_STYLE_ASSIGNMENT (( #13315 ) ) ;
#34806=SURFACE_STYLE_FILL_AREA ( #3089 ) ;
#34820=ORIENTED_EDGE ( 'NONE', *, *, #3890, .T. ) ;
#34825=VERTEX_POINT ( 'NONE', #17799 ) ;
#34853=ORIENTED_EDGE ( 'NONE', *, *, #12602, .F. ) ;
#34885=AXIS2_PLACEMENT_3D ( 'NONE', #19278, #24909, #46423 ) ;
#34999=SURFACE_STYLE_FILL_AREA ( #49200 ) ;
#35023=( NAMED_UNIT ( * ) SI_UNIT ( $, .STERADIAN. ) SOLID_ANGLE_UNIT ( ) );
#35029=ADVANCED_FACE ( 'NONE', ( #67360 ), #61377, .F. ) ;
#35131=FILL_AREA_STYLE_COLOUR ( '', #26968 ) ;
#35314=EDGE_CURVE ( 'NONE', #40876, #51672, #6112, .T. ) ;
#35349=( LENGTH_UNIT ( ) NAMED_UNIT ( * ) SI_UNIT ( .MILLI., .METRE. ) );
#35397=CARTESIAN_POINT ( 'NONE',  ( -12.94269599874522214, 56.39257344741367461, 6.552927311739624727 ) ) ;
#35445=AXIS2_PLACEMENT_3D ( 'NONE', #15922, #53528, #69026 ) ;
#35522=AXIS2_PLACEMENT_3D ( 'NONE', #33313, #32589, #17824 ) ;
#35637=UNCERTAINTY_MEASURE_WITH_UNIT (LENGTH_MEASURE( 1.000000000000000082E-05 ), #55967, 'distance_accuracy_value', 'NONE');
#35799=CARTESIAN_POINT ( 'NONE',  ( -16.72057948583355369, 65.79671608775228719, -5.561181121879805289 ) ) ;
#36010=STYLED_ITEM ( 'NONE', ( #50282 ), #11369 ) ;
#36041=ORIENTED_EDGE ( 'NONE', *, *, #44287, .T. ) ;
#36049=CARTESIAN_POINT ( 'NONE',  ( 6.999798566743343997, 9.396926207859090496, 11.50901484383454942 ) ) ;
#36226=CARTESIAN_POINT ( 'NONE',  ( 1.999798566743339334, 49.09558629977726696, 2.000000000000000000 ) ) ;
#36325=DIRECTION ( 'NONE',  ( 1.000000000000000000, -0.000000000000000000, -0.000000000000000000 ) ) ;
#36569=FILL_AREA_STYLE ('',( #63923 ) ) ;
#36574=VERTEX_POINT ( 'NONE', #34075 ) ;
#36582=EDGE_LOOP ( 'NONE', ( #45841, #39361, #2100, #41972 ) ) ;
#36723=CARTESIAN_POINT ( 'NONE',  ( -10.11618306975752368, 54.14354156754873060, -2.000000000000000000 ) ) ;
#36772=DIRECTION ( 'NONE',  ( -0.000000000000000000, -0.000000000000000000, -1.000000000000000000 ) ) ;
#36807=EDGE_LOOP ( 'NONE', ( #7784, #58491, #21115, #42199 ) ) ;
#36841=UNCERTAINTY_MEASURE_WITH_UNIT (LENGTH_MEASURE( 1.000000000000000082E-05 ), #49351, 'distance_accuracy_value', 'NONE');
#36850=CARTESIAN_POINT ( 'NONE',  ( 8.256904162901424371, 56.03086067945960025, -6.591072975109653953 ) ) ;
#36898=PRESENTATION_STYLE_ASSIGNMENT (( #58315 ) ) ;
#37026=CARTESIAN_POINT ( 'NONE',  ( 0.04677136509298115974, 68.99999999999998579, -6.349999999999994316 ) ) ;
#37040=ORIENTED_EDGE ( 'NONE', *, *, #17608, .T. ) ;
#37228=COLOUR_RGB ( '', 0.66274510, 0.83137255, 0.94901961) ;
#37254=PLANE ( 'NONE',  #48659 ) ;
#37281=FACE_OUTER_BOUND ( 'NONE', #6784, .T. ) ;
#37325=CARTESIAN_POINT ( 'NONE',  ( 1.999798566743339334, 49.09558629977726696, -2.000000000000000000 ) ) ;
#37328=( NAMED_UNIT ( * ) SI_UNIT ( $, .STERADIAN. ) SOLID_ANGLE_UNIT ( ) );
#37422=MECHANICAL_DESIGN_GEOMETRIC_PRESENTATION_REPRESENTATION('',(#62044),#19383);
#37674=SURFACE_SIDE_STYLE ('',( #21795 ) ) ;
#37727=EDGE_CURVE ( 'NONE', #69365, #40929, #31421, .T. ) ;
#37753=DIRECTION ( 'NONE',  ( -1.000000000000000000, 0.000000000000000000, 0.000000000000000000 ) ) ;
#37794=EDGE_CURVE ( 'NONE', #52209, #59509, #21942, .T. ) ;
#37878=DIRECTION ( 'NONE',  ( -1.000000000000000000, 0.000000000000000000, 0.000000000000000000 ) ) ;
#37920=( GEOMETRIC_REPRESENTATION_CONTEXT ( 3 ) GLOBAL_UNCERTAINTY_ASSIGNED_CONTEXT ( ( #68425 ) ) GLOBAL_UNIT_ASSIGNED_CONTEXT ( ( #34656, #22742, #52870 ) ) REPRESENTATION_CONTEXT ( 'NONE', 'WORKASPACE' ) );
#37930=FILL_AREA_STYLE_COLOUR ( '', #25777 ) ;
#38022=ORIENTED_EDGE ( 'NONE', *, *, #8185, .T. ) ;
#38036=( NAMED_UNIT ( * ) SI_UNIT ( $, .STERADIAN. ) SOLID_ANGLE_UNIT ( ) );
#38076=CARTESIAN_POINT ( 'NONE',  ( -20.08870137916957788, 4.181554945440833393, -12.05901974869650850 ) ) ;
#38119=( GEOMETRIC_REPRESENTATION_CONTEXT ( 3 ) GLOBAL_UNCERTAINTY_ASSIGNED_CONTEXT ( ( #21445 ) ) GLOBAL_UNIT_ASSIGNED_CONTEXT ( ( #59607, #48768, #468 ) ) REPRESENTATION_CONTEXT ( 'NONE', 'WORKASPACE' ) );
#38148=DIRECTION ( 'NONE',  ( -0.07898106964430656740, -0.9968761159932768567, -0.000000000000000000 ) ) ;
#38166=DIRECTION ( 'NONE',  ( 1.000000000000000000, 9.811390859391774840E-17, 0.000000000000000000 ) ) ;
#38305=CARTESIAN_POINT ( 'NONE',  ( 3.046771365092978190, 72.00000000000001421, 6.349999999999997868 ) ) ;
#38364=SURFACE_SIDE_STYLE ('',( #22485 ) ) ;
#38398=FILL_AREA_STYLE ('',( #16916 ) ) ;
#38408=DIRECTION ( 'NONE',  ( -0.000000000000000000, 0.000000000000000000, 1.000000000000000000 ) ) ;
#38441=( BOUNDED_CURVE ( )  B_SPLINE_CURVE ( 3, ( #69182, #36850, #64225, #26580 ),
 .UNSPECIFIED., .F., .F. ) 
 B_SPLINE_CURVE_WITH_KNOTS ( ( 4, 4 ),
 ( 3.919743979054040484, 4.712388980384689674 ),
 .UNSPECIFIED. ) 
 CURVE ( )  GEOMETRIC_REPRESENTATION_ITEM ( )  RATIONAL_B_SPLINE_CURVE ( ( 1.000000000000000000, 0.9483245655077794378, 0.9483245655077794378, 1.000000000000000000 ) ) 
 REPRESENTATION_ITEM ( '' )  );
#38520=( NAMED_UNIT ( * ) SI_UNIT ( $, .STERADIAN. ) SOLID_ANGLE_UNIT ( ) );
#38564=VECTOR ( 'NONE', #58410, 1000.000000000000227 ) ;
#38573=SURFACE_SIDE_STYLE ('',( #3522 ) ) ;
#38616=FACE_OUTER_BOUND ( 'NONE', #32423, .T. ) ;
#38627=PLANE ( 'NONE',  #35522 ) ;
#38718=MECHANICAL_DESIGN_GEOMETRIC_PRESENTATION_REPRESENTATION('',(#20536),#24058);
#38719=ADVANCED_FACE ( 'NONE', ( #59732 ), #6266, .T. ) ;
#38786=VECTOR ( 'NONE', #56848, 1000.000000000000227 ) ;
#38803=PRESENTATION_STYLE_ASSIGNMENT (( #55634 ) ) ;
#38829=CARTESIAN_POINT ( 'NONE',  ( 0.000000000000000000, 8.270287287112621792E-15, 12.50000000000000000 ) ) ;
#38974=( NAMED_UNIT ( * ) SI_UNIT ( $, .STERADIAN. ) SOLID_ANGLE_UNIT ( ) );
#38999=DIRECTION ( 'NONE',  ( 0.000000000000000000, 1.000000000000000000, 1.734723475976805615E-16 ) ) ;
#39045=CARTESIAN_POINT ( 'NONE',  ( -11.24540022918535698, 52.49282396394303873, 2.000000000000000000 ) ) ;
#39096=SURFACE_STYLE_USAGE ( .BOTH. , #56261 ) ;
#39166=LINE ( 'NONE', #38829, #13253 ) ;
#39184=ORIENTED_EDGE ( 'NONE', *, *, #26275, .T. ) ;
#39288=VECTOR ( 'NONE', #2123, 1000.000000000000114 ) ;
#39311=ORIENTED_EDGE ( 'NONE', *, *, #13427, .F. ) ;
#39340=VECTOR ( 'NONE', #13428, 1000.000000000000000 ) ;
#39361=ORIENTED_EDGE ( 'NONE', *, *, #44823, .F. ) ;
#39415=LINE ( 'NONE', #61178, #67219 ) ;
#39427=COLOUR_RGB ( '', 0.66274510, 0.83137255, 0.94901961) ;
#39433=ORIENTED_EDGE ( 'NONE', *, *, #60913, .T. ) ;
#39439=PRESENTATION_STYLE_ASSIGNMENT (( #39096 ) ) ;
#39532=CARTESIAN_POINT ( 'NONE',  ( -13.23915246117191025, 52.65078610323165265, 2.000000000000000000 ) ) ;
#39597=CIRCLE ( 'NONE', #67684, 1.999999999999998224 ) ;
#39612=DIRECTION ( 'NONE',  ( 0.000000000000000000, 0.000000000000000000, -1.000000000000000000 ) ) ;
#39616=ORIENTED_EDGE ( 'NONE', *, *, #8105, .T. ) ;
#39637=DIRECTION ( 'NONE',  ( -1.000000000000000000, 0.000000000000000000, 0.000000000000000000 ) ) ;
#39683=COLOUR_RGB ( '', 0.72549020, 0.75294118, 0.79215686) ;
#39752=SURFACE_SIDE_STYLE ('',( #45728 ) ) ;
#39828=ORIENTED_EDGE ( 'NONE', *, *, #43453, .T. ) ;
#39861=FACE_OUTER_BOUND ( 'NONE', #26224, .T. ) ;
#39915=CARTESIAN_POINT ( 'NONE',  ( -10.11618306975752368, 54.14354156754873060, -2.000000000000000000 ) ) ;
#39945=ORIENTED_EDGE ( 'NONE', *, *, #32139, .T. ) ;
#39977=PRESENTATION_STYLE_ASSIGNMENT (( #30061 ) ) ;
#39991=FILL_AREA_STYLE_COLOUR ( '', #54679 ) ;
#39994=FACE_OUTER_BOUND ( 'NONE', #22974, .T. ) ;
#40027=COLOUR_RGB ( '', 0.08235294, 0.09019608, 0.10196078) ;
#40072=ORIENTED_EDGE ( 'NONE', *, *, #6942, .T. ) ;
#40099=( NAMED_UNIT ( * ) PLANE_ANGLE_UNIT ( ) SI_UNIT ( $, .RADIAN. ) );
#40131=( LENGTH_UNIT ( ) NAMED_UNIT ( * ) SI_UNIT ( .MILLI., .METRE. ) );
#40150=DIRECTION ( 'NONE',  ( -0.000000000000000000, -0.000000000000000000, 1.000000000000000000 ) ) ;
#40171=FACE_OUTER_BOUND ( 'NONE', #47321, .T. ) ;
#40240=VECTOR ( 'NONE', #9207, 1000.000000000000000 ) ;
#40308=SURFACE_SIDE_STYLE ('',( #7929 ) ) ;
#40312=CARTESIAN_POINT ( 'NONE',  ( -20.42000000000000881, -1.426810058990923835E-13, 12.50000000000000000 ) ) ;
#40319=SURFACE_SIDE_STYLE ('',( #8311 ) ) ;
#40379=ADVANCED_FACE ( 'NONE', ( #29012, #66684 ), #13196, .F. ) ;
#40396=CARTESIAN_POINT ( 'NONE',  ( -13.23915246117191025, 52.65078610323165265, 2.000000000000000000 ) ) ;
#40399=DIRECTION ( 'NONE',  ( -1.000000000000000000, -1.224646799147353454E-16, 0.000000000000000000 ) ) ;
#40429=ORIENTED_EDGE ( 'NONE', *, *, #50753, .F. ) ;
#40468=ORIENTED_EDGE ( 'NONE', *, *, #44051, .T. ) ;
#40542=( GEOMETRIC_REPRESENTATION_CONTEXT ( 3 ) GLOBAL_UNCERTAINTY_ASSIGNED_CONTEXT ( ( #66530 ) ) GLOBAL_UNIT_ASSIGNED_CONTEXT ( ( #56585, #40099, #34437 ) ) REPRESENTATION_CONTEXT ( 'NONE', 'WORKASPACE' ) );
#40596=VERTEX_POINT ( 'NONE', #34157 ) ;
#40651=( LENGTH_UNIT ( ) NAMED_UNIT ( * ) SI_UNIT ( .MILLI., .METRE. ) );
#40760=EDGE_CURVE ( 'NONE', #60757, #21935, #64699, .T. ) ;
#40765=CARTESIAN_POINT ( 'NONE',  ( 3.999798566743339556, 49.09558629977726696, -2.000000000000000000 ) ) ;
#40840=SURFACE_STYLE_USAGE ( .BOTH. , #18981 ) ;
#40876=VERTEX_POINT ( 'NONE', #25663 ) ;
#40893=( NAMED_UNIT ( * ) SI_UNIT ( $, .STERADIAN. ) SOLID_ANGLE_UNIT ( ) );
#40929=VERTEX_POINT ( 'NONE', #69620 ) ;
#40959=AXIS2_PLACEMENT_3D ( 'NONE', #52327, #3722, #4420 ) ;
#41111=CARTESIAN_POINT ( 'NONE',  ( 3.062509476195515228E-31, -2.500728763858896269E-15, -12.50000000000000000 ) ) ;
#41116=SURFACE_STYLE_USAGE ( .BOTH. , #46761 ) ;
#41119=FILL_AREA_STYLE ('',( #30156 ) ) ;
#41138=SURFACE_STYLE_USAGE ( .BOTH. , #39752 ) ;
#41212=EDGE_LOOP ( 'NONE', ( #3279, #43937, #25476, #19801, #39433, #33385, #55767, #4267, #31823, #49748, #64541, #2857, #59424 ) ) ;
#41237=LINE ( 'NONE', #14460, #40240 ) ;
#41274=EDGE_CURVE ( 'NONE', #3117, #60568, #67455, .T. ) ;
#41282=ORIENTED_EDGE ( 'NONE', *, *, #44535, .T. ) ;
#41371=DIRECTION ( 'NONE',  ( -0.000000000000000000, -0.000000000000000000, -1.000000000000000000 ) ) ;
#41422=AXIS2_PLACEMENT_3D ( 'NONE', #61846, #19974, #62887 ) ;
#41453=DIRECTION ( 'NONE',  ( -1.000000000000000000, -1.074176415464006764E-16, 0.000000000000000000 ) ) ;
#41468=DIRECTION ( 'NONE',  ( 1.224646799147353454E-16, -1.000000000000000000, 0.000000000000000000 ) ) ;
#41525=AXIS2_PLACEMENT_3D ( 'NONE', #19530, #30077, #39637 ) ;
#41567=CARTESIAN_POINT ( 'NONE',  ( 3.999798566743339556, 8.867945265733707672, -12.50000000000000000 ) ) ;
#41625=AXIS2_PLACEMENT_3D ( 'NONE', #51587, #13953, #18859 ) ;
#41632=LINE ( 'NONE', #36723, #45744 ) ;
#41672=CIRCLE ( 'NONE', #42796, 5.000000000000004441 ) ;
#41714=CARTESIAN_POINT ( 'NONE',  ( -11.54296011127659050, 55.11956624581093678, 6.687176662279907369 ) ) ;
#41725=CARTESIAN_POINT ( 'NONE',  ( 17.15973193263811680, -3.000000000000000000, -12.50000000000000000 ) ) ;
#41797=DIRECTION ( 'NONE',  ( 0.3403530053317448401, -0.9351121967924955758, 0.09861547125863370789 ) ) ;
#41881=ORIENTED_EDGE ( 'NONE', *, *, #9488, .T. ) ;
#41966=COLOUR_RGB ( '', 0.08235294, 0.09019608, 0.10196078) ;
#41972=ORIENTED_EDGE ( 'NONE', *, *, #40760, .F. ) ;
#42057=DIRECTION ( 'NONE',  ( -0.000000000000000000, -0.000000000000000000, -1.000000000000000000 ) ) ;
#42097=LINE ( 'NONE', #63822, #7198 ) ;
#42103=CARTESIAN_POINT ( 'NONE',  ( 0.04677136509298115974, 68.99999999999998579, -2.000000000000000000 ) ) ;
#42166=MECHANICAL_DESIGN_GEOMETRIC_PRESENTATION_REPRESENTATION('',(#15194),#18511);
#42181=VERTEX_POINT ( 'NONE', #52371 ) ;
#42183=DIRECTION ( 'NONE',  ( -0.000000000000000000, -0.000000000000000000, -1.000000000000000000 ) ) ;
#42199=ORIENTED_EDGE ( 'NONE', *, *, #34391, .T. ) ;
#42212=AXIS2_PLACEMENT_3D ( 'NONE', #27998, #17166, #5507 ) ;
#42274=CYLINDRICAL_SURFACE ( 'NONE', #8532, 17.99999999999999645 ) ;
#42278=LINE ( 'NONE', #4914, #5955 ) ;
#42291=VERTEX_POINT ( 'NONE', #64633 ) ;
#42390=VERTEX_POINT ( 'NONE', #33649 ) ;
#42400=ORIENTED_EDGE ( 'NONE', *, *, #56448, .T. ) ;
#42457=EDGE_CURVE ( 'NONE', #40929, #59357, #50538, .T. ) ;
#42549=PLANE ( 'NONE',  #20307 ) ;
#42559=CARTESIAN_POINT ( 'NONE',  ( 8.046771365092977746, 72.00000000000001421, 12.50000000000000000 ) ) ;
#42587=ORIENTED_EDGE ( 'NONE', *, *, #23658, .T. ) ;
#42596=VERTEX_POINT ( 'NONE', #13933 ) ;
#42608=ORIENTED_EDGE ( 'NONE', *, *, #35314, .F. ) ;
#42647=ORIENTED_EDGE ( 'NONE', *, *, #55366, .F. ) ;
#42685=CARTESIAN_POINT ( 'NONE',  ( 10.57623092156539535, 58.31681314173471975, 6.349999999999996092 ) ) ;
#42711=CIRCLE ( 'NONE', #52767, 17.99999999999999645 ) ;
#42765=SURFACE_STYLE_FILL_AREA ( #67 ) ;
#42775=CARTESIAN_POINT ( 'NONE',  ( 17.15973193263811680, -3.000000000000000000, -2.000000000000000000 ) ) ;
#42796=AXIS2_PLACEMENT_3D ( 'NONE', #38305, #59707, #38999 ) ;
#42840=AXIS2_PLACEMENT_3D ( 'NONE', #59977, #7217, #49786 ) ;
#42859=STYLED_ITEM ( 'NONE', ( #61037 ), #45582 ) ;
#42865=COLOUR_RGB ( '', 0.40784314, 0.44705882, 0.49803922) ;
#42895=( GEOMETRIC_REPRESENTATION_CONTEXT ( 3 ) GLOBAL_UNCERTAINTY_ASSIGNED_CONTEXT ( ( #64318 ) ) GLOBAL_UNIT_ASSIGNED_CONTEXT ( ( #35349, #56804, #61019 ) ) REPRESENTATION_CONTEXT ( 'NONE', 'WORKASPACE' ) );
#42926=( NAMED_UNIT ( * ) SI_UNIT ( $, .STERADIAN. ) SOLID_ANGLE_UNIT ( ) );
#42948=FILL_AREA_STYLE_COLOUR ( '', #40027 ) ;
#42982=CARTESIAN_POINT ( 'NONE',  ( 3.999798566743338668, 49.09558629977726696, -7.322456175549363344 ) ) ;
#42983=SURFACE_STYLE_USAGE ( .BOTH. , #58767 ) ;
#43026=( LENGTH_UNIT ( ) NAMED_UNIT ( * ) SI_UNIT ( .MILLI., .METRE. ) );
#43112=( NAMED_UNIT ( * ) SI_UNIT ( $, .STERADIAN. ) SOLID_ANGLE_UNIT ( ) );
#43152=SURFACE_STYLE_USAGE ( .BOTH. , #789 ) ;
#43218=ORIENTED_EDGE ( 'NONE', *, *, #10653, .T. ) ;
#43258=SURFACE_STYLE_USAGE ( .BOTH. , #48520 ) ;
#43262=PRESENTATION_STYLE_ASSIGNMENT (( #51691 ) ) ;
#43281=EDGE_CURVE ( 'NONE', #53207, #2615, #56004, .T. ) ;
#43342=CARTESIAN_POINT ( 'NONE',  ( 3.062992266794108520, 51.20951172609373003, -7.099524902877636379 ) ) ;
#43383=FILL_AREA_STYLE ('',( #11302 ) ) ;
#43394=ORIENTED_EDGE ( 'NONE', *, *, #54782, .F. ) ;
#43453=EDGE_CURVE ( 'NONE', #33557, #42181, #39415, .T. ) ;
#43499=VERTEX_POINT ( 'NONE', #60814 ) ;
#43553=ORIENTED_EDGE ( 'NONE', *, *, #62862, .T. ) ;
#43569=ORIENTED_EDGE ( 'NONE', *, *, #9365, .T. ) ;
#43635=FILL_AREA_STYLE ('',( #32678 ) ) ;
#43753=FACE_OUTER_BOUND ( 'NONE', #7112, .T. ) ;
#43757=SURFACE_SIDE_STYLE ('',( #55659 ) ) ;
#43775=CIRCLE ( 'NONE', #2088, 15.00000000000000000 ) ;
#43782=SURFACE_STYLE_USAGE ( .BOTH. , #50758 ) ;
#43856=VECTOR ( 'NONE', #13079, 1000.000000000000000 ) ;
#43903=SURFACE_SIDE_STYLE ('',( #48482 ) ) ;
#43937=ORIENTED_EDGE ( 'NONE', *, *, #44287, .F. ) ;
#43967=DIRECTION ( 'NONE',  ( -1.000000000000000000, 0.000000000000000000, 0.000000000000000000 ) ) ;
#43999=( GEOMETRIC_REPRESENTATION_CONTEXT ( 3 ) GLOBAL_UNCERTAINTY_ASSIGNED_CONTEXT ( ( #35637 ) ) GLOBAL_UNIT_ASSIGNED_CONTEXT ( ( #55967, #67220, #45117 ) ) REPRESENTATION_CONTEXT ( 'NONE', 'WORKASPACE' ) );
#44051=EDGE_CURVE ( 'NONE', #69365, #22057, #26140, .T. ) ;
#44099=( BOUNDED_CURVE ( )  B_SPLINE_CURVE ( 3, ( #58415, #43342, #30982, #42982 ),
 .UNSPECIFIED., .F., .F. ) 
 B_SPLINE_CURVE_WITH_KNOTS ( ( 4, 4 ),
 ( 3.043785426622117374, 4.712388980384689674 ),
 .UNSPECIFIED. ) 
 CURVE ( )  GEOMETRIC_REPRESENTATION_ITEM ( )  RATIONAL_B_SPLINE_CURVE ( ( 1.000000000000000000, 0.7811300729168891843, 0.7811300729168891843, 1.000000000000000000 ) ) 
 REPRESENTATION_ITEM ( '' )  );
#44129=ADVANCED_FACE ( 'NONE', ( #43753 ), #27844, .F. ) ;
#44287=EDGE_CURVE ( 'NONE', #1680, #17724, #29247, .T. ) ;
#44369=SURFACE_STYLE_USAGE ( .BOTH. , #49607 ) ;
#44438=DIRECTION ( 'NONE',  ( -1.000000000000000000, 0.000000000000000000, 0.000000000000000000 ) ) ;
#44531=LINE ( 'NONE', #1508, #65017 ) ;
#44535=EDGE_CURVE ( 'NONE', #59509, #47453, #10929, .T. ) ;
#44744=ORIENTED_EDGE ( 'NONE', *, *, #64011, .T. ) ;
#44788=SURFACE_STYLE_FILL_AREA ( #1781 ) ;
#44823=EDGE_CURVE ( 'NONE', #26409, #45813, #6748, .T. ) ;
#44849=VERTEX_POINT ( 'NONE', #14050 ) ;
#44875=VERTEX_POINT ( 'NONE', #57295 ) ;
#44906=STYLED_ITEM ( 'NONE', ( #26805 ), #44129 ) ;
#44928=CYLINDRICAL_SURFACE ( 'NONE', #41525, 17.42000000000001236 ) ;
#44998=AXIS2_PLACEMENT_3D ( 'NONE', #26991, #11184, #26317 ) ;
#45000=FILL_AREA_STYLE ('',( #33030 ) ) ;
#45003=( BOUNDED_CURVE ( )  B_SPLINE_CURVE ( 3, ( #17002, #26098, #4271, #42685 ),
 .UNSPECIFIED., .F., .F. ) 
 B_SPLINE_CURVE_WITH_KNOTS ( ( 4, 4 ),
 ( 4.712388980384689674, 5.505033981715339308 ),
 .UNSPECIFIED. ) 
 CURVE ( )  GEOMETRIC_REPRESENTATION_ITEM ( )  RATIONAL_B_SPLINE_CURVE ( ( 1.000000000000000000, 0.9483245655077793268, 0.9483245655077793268, 1.000000000000000000 ) ) 
 REPRESENTATION_ITEM ( '' )  );
#45035=CARTESIAN_POINT ( 'NONE',  ( 1.804495846578303864, 51.08602766979955589, 7.112547338523483198 ) ) ;
#45058=CARTESIAN_POINT ( 'NONE',  ( 0.000000000000000000, 0.000000000000000000, -12.50000000000000000 ) ) ;
#45061=VECTOR ( 'NONE', #41797, 999.9999999999998863 ) ;
#45117=( NAMED_UNIT ( * ) SI_UNIT ( $, .STERADIAN. ) SOLID_ANGLE_UNIT ( ) );
#45122=( GEOMETRIC_REPRESENTATION_CONTEXT ( 3 ) GLOBAL_UNCERTAINTY_ASSIGNED_CONTEXT ( ( #27732 ) ) GLOBAL_UNIT_ASSIGNED_CONTEXT ( ( #31237, #47133, #21386 ) ) REPRESENTATION_CONTEXT ( 'NONE', 'WORKASPACE' ) );
#45159=EDGE_CURVE ( 'NONE', #63718, #20985, #10178, .T. ) ;
#45260=CLOSED_SHELL ( 'NONE', ( #27916, #59678, #15523, #55549, #22970, #19005, #64881, #46620, #14785, #38719, #11369, #40379, #15173, #68155, #44129, #30884, #17106, #3359, #2318, #55422, #58288, #56958, #35029, #13616, #662, #7231, #30079, #45582, #31183, #56708, #1136, #62317, #29512 ) ) ;
#45318=EDGE_CURVE ( 'NONE', #1680, #29661, #27105, .T. ) ;
#45395=CARTESIAN_POINT ( 'NONE',  ( 8.046771365092977746, 72.00000000000001421, -6.349999999999997868 ) ) ;
#45397=EDGE_CURVE ( 'NONE', #52209, #18031, #13368, .T. ) ;
#45498=FACE_OUTER_BOUND ( 'NONE', #54705, .T. ) ;
#45582=ADVANCED_FACE ( 'NONE', ( #5834 ), #27273, .T. ) ;
#45589=LINE ( 'NONE', #9309, #54062 ) ;
#45623=DIRECTION ( 'NONE',  ( 0.9396926207859093161, 0.3420201433256664370, 0.000000000000000000 ) ) ;
#45683=COLOUR_RGB ( '', 0.08235294, 0.09019608, 0.10196078) ;
#45694=ORIENTED_EDGE ( 'NONE', *, *, #19604, .F. ) ;
#45708=SURFACE_STYLE_FILL_AREA ( #41119 ) ;
#45728=SURFACE_STYLE_FILL_AREA ( #24222 ) ;
#45730=DIRECTION ( 'NONE',  ( -0.000000000000000000, -0.000000000000000000, 1.000000000000000000 ) ) ;
#45744=VECTOR ( 'NONE', #47274, 1000.000000000000000 ) ;
#45755=FACE_OUTER_BOUND ( 'NONE', #54363, .T. ) ;
#45766=ORIENTED_EDGE ( 'NONE', *, *, #26275, .F. ) ;
#45780=ORIENTED_EDGE ( 'NONE', *, *, #67094, .F. ) ;
#45791=ORIENTED_EDGE ( 'NONE', *, *, #62862, .F. ) ;
#45813=VERTEX_POINT ( 'NONE', #53614 ) ;
#45841=ORIENTED_EDGE ( 'NONE', *, *, #33208, .F. ) ;
#45903=AXIS2_PLACEMENT_3D ( 'NONE', #58765, #32032, #5977 ) ;
#45953=LINE ( 'NONE', #41725, #69581 ) ;
#45998=EDGE_CURVE ( 'NONE', #11115, #40876, #45003, .T. ) ;
#46000=DIRECTION ( 'NONE',  ( -0.000000000000000000, -0.000000000000000000, 1.000000000000000000 ) ) ;
#46087=UNCERTAINTY_MEASURE_WITH_UNIT (LENGTH_MEASURE( 1.000000000000000082E-05 ), #61542, 'distance_accuracy_value', 'NONE');
#46162=VECTOR ( 'NONE', #29556, 1000.000000000000227 ) ;
#46210=MECHANICAL_DESIGN_GEOMETRIC_PRESENTATION_REPRESENTATION('',(#42859),#60753);
#46211=CARTESIAN_POINT ( 'NONE',  ( -10.11618306975752368, 54.14354156754873060, 6.790106699912857202 ) ) ;
#46423=DIRECTION ( 'NONE',  ( 1.000000000000000000, 0.000000000000000000, 0.000000000000000000 ) ) ;
#46574=CARTESIAN_POINT ( 'NONE',  ( 10.57623092156539357, 58.31681314173471975, 12.50000000000000000 ) ) ;
#46603=STYLED_ITEM ( 'NONE', ( #63200 ), #30079 ) ;
#46620=ADVANCED_FACE ( 'NONE', ( #9432 ), #3391, .F. ) ;
#46675=( LENGTH_UNIT ( ) NAMED_UNIT ( * ) SI_UNIT ( .MILLI., .METRE. ) );
#46685=EDGE_CURVE ( 'NONE', #34272, #40596, #62522, .T. ) ;
#46761=SURFACE_SIDE_STYLE ('',( #57608 ) ) ;
#46803=DIRECTION ( 'NONE',  ( 0.000000000000000000, -0.9944852160011111719, -0.1048768571002353378 ) ) ;
#46838=VERTEX_POINT ( 'NONE', #39915 ) ;
#46852=UNCERTAINTY_MEASURE_WITH_UNIT (LENGTH_MEASURE( 1.000000000000000082E-05 ), #30764, 'distance_accuracy_value', 'NONE');
#46887=DIRECTION ( 'NONE',  ( 0.000000000000000000, 1.000000000000000000, 1.350863103983176297E-16 ) ) ;
#47083=DIRECTION ( 'NONE',  ( 0.3403530053317450621, -0.9351121967924954648, -0.09861547125863368013 ) ) ;
#47088=( NAMED_UNIT ( * ) PLANE_ANGLE_UNIT ( ) SI_UNIT ( $, .RADIAN. ) );
#47108=SURFACE_SIDE_STYLE ('',( #14726 ) ) ;
#47133=( NAMED_UNIT ( * ) PLANE_ANGLE_UNIT ( ) SI_UNIT ( $, .RADIAN. ) );
#47227=CARTESIAN_POINT ( 'NONE',  ( 0.000000000000000000, 0.000000000000000000, -2.000000000000000000 ) ) ;
#47274=DIRECTION ( 'NONE',  ( -0.000000000000000000, -0.000000000000000000, -1.000000000000000000 ) ) ;
#47321=EDGE_LOOP ( 'NONE', ( #33352, #37040, #40429, #34853 ) ) ;
#47446=EDGE_LOOP ( 'NONE', ( #4219, #852, #14561, #24908 ) ) ;
#47453=VERTEX_POINT ( 'NONE', #16896 ) ;
#47485=CARTESIAN_POINT ( 'NONE',  ( 7.227466682572271317, 6.938893903907228378E-15, 12.50000000000000000 ) ) ;
#47541=CYLINDRICAL_SURFACE ( 'NONE', #27605, 2.000000000000003553 ) ;
#47548=DIRECTION ( 'NONE',  ( 1.000000000000000000, 0.000000000000000000, 0.000000000000000000 ) ) ;
#47586=LINE ( 'NONE', #9905, #22247 ) ;
#47642=EDGE_CURVE ( 'NONE', #13821, #18031, #24211, .T. ) ;
#47754=CYLINDRICAL_SURFACE ( 'NONE', #4340, 12.00000000000000178 ) ;
#47768=DIRECTION ( 'NONE',  ( 1.068252564556022042E-16, -0.9944852160011111719, 0.1048768571002353378 ) ) ;
#47772=EDGE_CURVE ( 'NONE', #23615, #34825, #54407, .T. ) ;
#47773=CARTESIAN_POINT ( 'NONE',  ( 3.999798566743338668, 58.31681314173471975, -6.349999999999996092 ) ) ;
#47803=ORIENTED_EDGE ( 'NONE', *, *, #25563, .T. ) ;
#47860=( GEOMETRIC_REPRESENTATION_CONTEXT ( 3 ) GLOBAL_UNCERTAINTY_ASSIGNED_CONTEXT ( ( #65784 ) ) GLOBAL_UNIT_ASSIGNED_CONTEXT ( ( #43026, #27106, #32072 ) ) REPRESENTATION_CONTEXT ( 'NONE', 'WORKASPACE' ) );
#48016=CARTESIAN_POINT ( 'NONE',  ( -14.95322863490702225, 69.00000000000000000, 12.50000000000000000 ) ) ;
#48065=CARTESIAN_POINT ( 'NONE',  ( -17.41962728626436530, -0.1139526552317604857, -2.000000000000000000 ) ) ;
#48077=FILL_AREA_STYLE ('',( #64887 ) ) ;
#48192=CYLINDRICAL_SURFACE ( 'NONE', #48745, 2.000000000000003553 ) ;
#48216=DIRECTION ( 'NONE',  ( -0.000000000000000000, -0.000000000000000000, 1.000000000000000000 ) ) ;
#48217=ORIENTED_EDGE ( 'NONE', *, *, #56710, .T. ) ;
#48373=AXIS2_PLACEMENT_3D ( 'NONE', #36226, #57654, #50990 ) ;
#48482=SURFACE_STYLE_FILL_AREA ( #17501 ) ;
#48520=SURFACE_SIDE_STYLE ('',( #52733 ) ) ;
#48522=( NAMED_UNIT ( * ) PLANE_ANGLE_UNIT ( ) SI_UNIT ( $, .RADIAN. ) );
#48640=CARTESIAN_POINT ( 'NONE',  ( 3.999798566743339556, 49.09558629977726696, -2.000000000000000000 ) ) ;
#48659=AXIS2_PLACEMENT_3D ( 'NONE', #31569, #41468, #52374 ) ;
#48661=ORIENTED_EDGE ( 'NONE', *, *, #13865, .F. ) ;
#48688=STYLED_ITEM ( 'NONE', ( #66409 ), #22970 ) ;
#48734=VECTOR ( 'NONE', #36772, 1000.000000000000000 ) ;
#48745=AXIS2_PLACEMENT_3D ( 'NONE', #64324, #27357, #16858 ) ;
#48768=( NAMED_UNIT ( * ) PLANE_ANGLE_UNIT ( ) SI_UNIT ( $, .RADIAN. ) );
#48883=ORIENTED_EDGE ( 'NONE', *, *, #54782, .T. ) ;
#48886=VECTOR ( 'NONE', #8199, 1000.000000000000114 ) ;
#48929=UNCERTAINTY_MEASURE_WITH_UNIT (LENGTH_MEASURE( 1.000000000000000082E-05 ), #56602, 'distance_accuracy_value', 'NONE');
#48969=ORIENTED_EDGE ( 'NONE', *, *, #19604, .T. ) ;
#49020=MECHANICAL_DESIGN_GEOMETRIC_PRESENTATION_REPRESENTATION('',(#18651),#69217);
#49192=CARTESIAN_POINT ( 'NONE',  ( 10.57623092156537936, 58.31681314173471975, -6.349999999999996092 ) ) ;
#49200=FILL_AREA_STYLE ('',( #27697 ) ) ;
#49346=SURFACE_STYLE_FILL_AREA ( #59528 ) ;
#49351=( LENGTH_UNIT ( ) NAMED_UNIT ( * ) SI_UNIT ( .MILLI., .METRE. ) );
#49369=LINE ( 'NONE', #33523, #39288 ) ;
#49440=STYLED_ITEM ( 'NONE', ( #28552 ), #53933 ) ;
#49540=ORIENTED_EDGE ( 'NONE', *, *, #56710, .F. ) ;
#49607=SURFACE_SIDE_STYLE ('',( #59800 ) ) ;
#49738=VECTOR ( 'NONE', #12175, 1000.000000000000000 ) ;
#49748=ORIENTED_EDGE ( 'NONE', *, *, #51887, .F. ) ;
#49786=DIRECTION ( 'NONE',  ( 1.000000000000000000, 0.000000000000000000, 0.000000000000000000 ) ) ;
#49826=AXIS2_PLACEMENT_3D ( 'NONE', #25947, #52024, #3062 ) ;
#49846=DIRECTION ( 'NONE',  ( -0.000000000000000000, -0.000000000000000000, -1.000000000000000000 ) ) ;
#50018=ORIENTED_EDGE ( 'NONE', *, *, #69568, .F. ) ;
#50064=EDGE_LOOP ( 'NONE', ( #4110, #49540, #21960, #67436 ) ) ;
#50189=LINE ( 'NONE', #27990, #2747 ) ;
#50282=PRESENTATION_STYLE_ASSIGNMENT (( #41138 ) ) ;
#50406=PRESENTATION_STYLE_ASSIGNMENT (( #43782 ) ) ;
#50479=SHAPE_DEFINITION_REPRESENTATION ( #20952, #31597 ) ;
#50538=LINE ( 'NONE', #6918, #65043 ) ;
#50621=PLANE ( 'NONE',  #34885 ) ;
#50623=LINE ( 'NONE', #8053, #7096 ) ;
#50636=( NAMED_UNIT ( * ) SI_UNIT ( $, .STERADIAN. ) SOLID_ANGLE_UNIT ( ) );
#50705=FILL_AREA_STYLE_COLOUR ( '', #15912 ) ;
#50713=ORIENTED_EDGE ( 'NONE', *, *, #66964, .T. ) ;
#50753=EDGE_CURVE ( 'NONE', #20985, #63718, #27835, .T. ) ;
#50758=SURFACE_SIDE_STYLE ('',( #28921 ) ) ;
#50844=DIRECTION ( 'NONE',  ( -0.000000000000000000, -0.000000000000000000, 1.000000000000000000 ) ) ;
#50951=PLANE ( 'NONE',  #21731 ) ;
#50971=( LENGTH_UNIT ( ) NAMED_UNIT ( * ) SI_UNIT ( .MILLI., .METRE. ) );
#50990=DIRECTION ( 'NONE',  ( 1.000000000000000000, 0.000000000000000000, 0.000000000000000000 ) ) ;
#50991=DIRECTION ( 'NONE',  ( -1.000000000000000000, -9.811390859391773608E-17, 0.000000000000000000 ) ) ;
#51197=CARTESIAN_POINT ( 'NONE',  ( 0.000000000000000000, 0.000000000000000000, 2.000000000000000000 ) ) ;
#51214=( NAMED_UNIT ( * ) PLANE_ANGLE_UNIT ( ) SI_UNIT ( $, .RADIAN. ) );
#51262=FILL_AREA_STYLE ('',( #8697 ) ) ;
#51293=LINE ( 'NONE', #34744, #27783 ) ;
#51397=EDGE_CURVE ( 'NONE', #51672, #4018, #43775, .T. ) ;
#51510=FILL_AREA_STYLE_COLOUR ( '', #21446 ) ;
#51585=UNCERTAINTY_MEASURE_WITH_UNIT (LENGTH_MEASURE( 1.000000000000000082E-05 ), #22731, 'distance_accuracy_value', 'NONE');
#51587=CARTESIAN_POINT ( 'NONE',  ( 0.000000000000000000, 0.000000000000000000, 2.000000000000000000 ) ) ;
#51595=MECHANICAL_DESIGN_GEOMETRIC_PRESENTATION_REPRESENTATION('',(#44906),#7803);
#51672=VERTEX_POINT ( 'NONE', #49192 ) ;
#51685=( GEOMETRIC_REPRESENTATION_CONTEXT ( 3 ) GLOBAL_UNCERTAINTY_ASSIGNED_CONTEXT ( ( #48929 ) ) GLOBAL_UNIT_ASSIGNED_CONTEXT ( ( #56602, #8066, #50636 ) ) REPRESENTATION_CONTEXT ( 'NONE', 'WORKASPACE' ) );
#51691=SURFACE_STYLE_USAGE ( .BOTH. , #30198 ) ;
#51707=DIRECTION ( 'NONE',  ( -0.000000000000000000, -0.000000000000000000, -1.000000000000000000 ) ) ;
#51819=UNCERTAINTY_MEASURE_WITH_UNIT (LENGTH_MEASURE( 1.000000000000000082E-05 ), #52654, 'distance_accuracy_value', 'NONE');
#51887=EDGE_CURVE ( 'NONE', #53696, #51899, #58960, .T. ) ;
#51894=ORIENTED_EDGE ( 'NONE', *, *, #60913, .F. ) ;
#51899=VERTEX_POINT ( 'NONE', #10773 ) ;
#51901=DIRECTION ( 'NONE',  ( 0.000000000000000000, 1.350863103983176297E-16, 1.000000000000000000 ) ) ;
#51949=EDGE_CURVE ( 'NONE', #40929, #33557, #16435, .T. ) ;
#51953=DIRECTION ( 'NONE',  ( -0.000000000000000000, 1.000000000000000000, -0.000000000000000000 ) ) ;
#52024=DIRECTION ( 'NONE',  ( -0.000000000000000000, -0.000000000000000000, 1.000000000000000000 ) ) ;
#52040=COLOUR_RGB ( '', 0.40784314, 0.44705882, 0.49803922) ;
#52068=CARTESIAN_POINT ( 'NONE',  ( 20.42000000000000526, 0.000000000000000000, -12.50000000000000000 ) ) ;
#52184=DIRECTION ( 'NONE',  ( 0.000000000000000000, 0.000000000000000000, 1.000000000000000000 ) ) ;
#52209=VERTEX_POINT ( 'NONE', #36049 ) ;
#52327=CARTESIAN_POINT ( 'NONE',  ( -11.24540022918535698, 52.49282396394303873, -2.000000000000000000 ) ) ;
#52331=AXIS2_PLACEMENT_3D ( 'NONE', #24604, #30579, #61907 ) ;
#52371=CARTESIAN_POINT ( 'NONE',  ( 3.999798566743335115, 8.867945265733711224, 11.56480034751363917 ) ) ;
#52373=ORIENTED_EDGE ( 'NONE', *, *, #35314, .T. ) ;
#52374=DIRECTION ( 'NONE',  ( 1.000000000000000000, 1.224646799147353454E-16, 0.000000000000000000 ) ) ;
#52403=UNCERTAINTY_MEASURE_WITH_UNIT (LENGTH_MEASURE( 1.000000000000000082E-05 ), #26838, 'distance_accuracy_value', 'NONE');
#52513=DIRECTION ( 'NONE',  ( 0.000000000000000000, -1.000000000000000000, 1.734723475976805615E-16 ) ) ;
#52588=DIRECTION ( 'NONE',  ( -1.000000000000000000, 0.000000000000000000, 0.000000000000000000 ) ) ;
#52654=( LENGTH_UNIT ( ) NAMED_UNIT ( * ) SI_UNIT ( .MILLI., .METRE. ) );
#52733=SURFACE_STYLE_FILL_AREA ( #9828 ) ;
#52736=VECTOR ( 'NONE', #26510, 1000.000000000000000 ) ;
#52767=AXIS2_PLACEMENT_3D ( 'NONE', #42103, #57888, #4369 ) ;
#52780=( NAMED_UNIT ( * ) PLANE_ANGLE_UNIT ( ) SI_UNIT ( $, .RADIAN. ) );
#52844=VECTOR ( 'NONE', #27258, 1000.000000000000000 ) ;
#52870=( NAMED_UNIT ( * ) SI_UNIT ( $, .STERADIAN. ) SOLID_ANGLE_UNIT ( ) );
#53042=CIRCLE ( 'NONE', #3578, 15.00000000000000000 ) ;
#53084=EDGE_CURVE ( 'NONE', #25644, #51899, #45589, .T. ) ;
#53172=CARTESIAN_POINT ( 'NONE',  ( -37.50000000000000000, 58.31681314173471975, 6.349999999999996092 ) ) ;
#53181=AXIS2_PLACEMENT_3D ( 'NONE', #39045, #12250, #28064 ) ;
#53196=FACE_OUTER_BOUND ( 'NONE', #36807, .T. ) ;
#53207=VERTEX_POINT ( 'NONE', #24086 ) ;
#53253=DIRECTION ( 'NONE',  ( -0.000000000000000000, -0.000000000000000000, -1.000000000000000000 ) ) ;
#53290=ORIENTED_EDGE ( 'NONE', *, *, #45998, .F. ) ;
#53303=LINE ( 'NONE', #25499, #65051 ) ;
#53368=ORIENTED_EDGE ( 'NONE', *, *, #55366, .T. ) ;
#53400=CARTESIAN_POINT ( 'NONE',  ( -16.72057948583355369, 65.79671608775228719, 5.561181121879805289 ) ) ;
#53528=DIRECTION ( 'NONE',  ( -0.000000000000000000, -0.000000000000000000, -1.000000000000000000 ) ) ;
#53576=( LENGTH_UNIT ( ) NAMED_UNIT ( * ) SI_UNIT ( .MILLI., .METRE. ) );
#53614=CARTESIAN_POINT ( 'NONE',  ( 1.804495846578303864, 51.08602766979955589, 2.000000000000000000 ) ) ;
#53696=VERTEX_POINT ( 'NONE', #66744 ) ;
#53703=CARTESIAN_POINT ( 'NONE',  ( 10.42000000000000526, 0.000000000000000000, 12.50000000000000000 ) ) ;
#53826=CARTESIAN_POINT ( 'NONE',  ( 6.999798566743344885, 2.607462097171131976, -12.22502112111942196 ) ) ;
#53860=PRESENTATION_STYLE_ASSIGNMENT (( #31354 ) ) ;
#53904=EDGE_CURVE ( 'NONE', #21935, #42181, #20274, .T. ) ;
#53918=COLOUR_RGB ( '', 0.31764706, 0.68627451, 0.89019608) ;
#53933=ADVANCED_BREP_SHAPE_REPRESENTATION ( '', ( #27320, #42840 ), #60796 ) ;
#53943=SURFACE_SIDE_STYLE ('',( #42765 ) ) ;
#54003=LINE ( 'NONE', #65254, #21965 ) ;
#54040=AXIS2_PLACEMENT_3D ( 'NONE', #55776, #1561, #34324 ) ;
#54054=FILL_AREA_STYLE_COLOUR ( '', #45683 ) ;
#54056=COLOUR_RGB ( '', 0.31764706, 0.68627451, 0.89019608) ;
#54062=VECTOR ( 'NONE', #30367, 1000.000000000000000 ) ;
#54094=PRODUCT ( '3. Padlock', '3. Padlock', '', ( #28990 ) ) ;
#54142=AXIS2_PLACEMENT_3D ( 'NONE', #45058, #22181, #66470 ) ;
#54278=LINE ( 'NONE', #11021, #57221 ) ;
#54363=EDGE_LOOP ( 'NONE', ( #56928, #7212, #3308, #7156, #16060, #60283, #2408, #16675 ) ) ;
#54407=LINE ( 'NONE', #27306, #49738 ) ;
#54433=MECHANICAL_DESIGN_GEOMETRIC_PRESENTATION_REPRESENTATION('',(#24114),#8420);
#54435=UNCERTAINTY_MEASURE_WITH_UNIT (LENGTH_MEASURE( 1.000000000000000082E-05 ), #33642, 'distance_accuracy_value', 'NONE');
#54455=( NAMED_UNIT ( * ) PLANE_ANGLE_UNIT ( ) SI_UNIT ( $, .RADIAN. ) );
#54466=( NAMED_UNIT ( * ) PLANE_ANGLE_UNIT ( ) SI_UNIT ( $, .RADIAN. ) );
#54492=ORIENTED_EDGE ( 'NONE', *, *, #6942, .F. ) ;
#54525=UNCERTAINTY_MEASURE_WITH_UNIT (LENGTH_MEASURE( 1.000000000000000082E-05 ), #17244, 'distance_accuracy_value', 'NONE');
#54679=COLOUR_RGB ( '', 0.31764706, 0.68627451, 0.89019608) ;
#54705=EDGE_LOOP ( 'NONE', ( #11273, #7587, #30595, #4521, #17643 ) ) ;
#54742=DIRECTION ( 'NONE',  ( 0.3403530053317450621, -0.9351121967924954648, 0.09861547125863368013 ) ) ;
#54782=EDGE_CURVE ( 'NONE', #42291, #3117, #39597, .T. ) ;
#54838=ORIENTED_EDGE ( 'NONE', *, *, #9365, .F. ) ;
#54961=PLANE ( 'NONE',  #22887 ) ;
#55022=DIRECTION ( 'NONE',  ( -0.9396926207859093161, -0.3420201433256664370, 0.000000000000000000 ) ) ;
#55077=ORIENTED_EDGE ( 'NONE', *, *, #3711, .F. ) ;
#55152=ORIENTED_EDGE ( 'NONE', *, *, #47642, .F. ) ;
#55176=MECHANICAL_DESIGN_GEOMETRIC_PRESENTATION_REPRESENTATION('',(#31588),#43999);
#55185=( NAMED_UNIT ( * ) PLANE_ANGLE_UNIT ( ) SI_UNIT ( $, .RADIAN. ) );
#55211=UNCERTAINTY_MEASURE_WITH_UNIT (LENGTH_MEASURE( 1.000000000000000082E-05 ), #26364, 'distance_accuracy_value', 'NONE');
#55228=CARTESIAN_POINT ( 'NONE',  ( 8.319377385370872346, -3.000000000000000888, -2.000000000000000000 ) ) ;
#55294=FACE_BOUND ( 'NONE', #3588, .T. ) ;
#55315=VECTOR ( 'NONE', #40399, 1000.000000000000000 ) ;
#55366=EDGE_CURVE ( 'NONE', #63828, #22057, #18331, .T. ) ;
#55376=EDGE_CURVE ( 'NONE', #44849, #443, #42278, .T. ) ;
#55422=ADVANCED_FACE ( 'NONE', ( #64711 ), #11231, .F. ) ;
#55549=ADVANCED_FACE ( 'NONE', ( #66786 ), #50951, .T. ) ;
#55617=EDGE_CURVE ( 'NONE', #25644, #44875, #55871, .T. ) ;
#55634=SURFACE_STYLE_USAGE ( .BOTH. , #8145 ) ;
#55649=PRESENTATION_STYLE_ASSIGNMENT (( #60909 ) ) ;
#55659=SURFACE_STYLE_FILL_AREA ( #33176 ) ;
#55767=ORIENTED_EDGE ( 'NONE', *, *, #7292, .F. ) ;
#55776=CARTESIAN_POINT ( 'NONE',  ( -13.23915246117191025, 52.65078610323165265, -2.000000000000000000 ) ) ;
#55871=LINE ( 'NONE', #40765, #68945 ) ;
#55887=CARTESIAN_POINT ( 'NONE',  ( 17.15973193263811680, -3.000000000000000000, -2.000000000000000000 ) ) ;
#55891=CARTESIAN_POINT ( 'NONE',  ( -6.588738478070744975, 51.73049953470015083, 7.044582342571018785 ) ) ;
#55903=DIRECTION ( 'NONE',  ( -0.000000000000000000, -0.000000000000000000, 1.000000000000000000 ) ) ;
#55967=( LENGTH_UNIT ( ) NAMED_UNIT ( * ) SI_UNIT ( .MILLI., .METRE. ) );
#56004=CIRCLE ( 'NONE', #45903, 5.000000000000004441 ) ;
#56205=SURFACE_SIDE_STYLE ('',( #45708 ) ) ;
#56261=SURFACE_SIDE_STYLE ('',( #34806 ) ) ;
#56280=EDGE_LOOP ( 'NONE', ( #45766, #43394, #19175, #604 ) ) ;
#56447=SURFACE_SIDE_STYLE ('',( #34999 ) ) ;
#56448=EDGE_CURVE ( 'NONE', #18730, #63828, #2509, .T. ) ;
#56473=UNCERTAINTY_MEASURE_WITH_UNIT (LENGTH_MEASURE( 1.000000000000000082E-05 ), #17388, 'distance_accuracy_value', 'NONE');
#56476=SURFACE_STYLE_USAGE ( .BOTH. , #40319 ) ;
#56520=CARTESIAN_POINT ( 'NONE',  ( 3.999798566743338668, 58.31681314173471975, 6.349999999999996092 ) ) ;
#56556=DIRECTION ( 'NONE',  ( -0.000000000000000000, -0.000000000000000000, -1.000000000000000000 ) ) ;
#56585=( LENGTH_UNIT ( ) NAMED_UNIT ( * ) SI_UNIT ( .MILLI., .METRE. ) );
#56602=( LENGTH_UNIT ( ) NAMED_UNIT ( * ) SI_UNIT ( .MILLI., .METRE. ) );
#56603=VECTOR ( 'NONE', #49846, 1000.000000000000000 ) ;
#56678=ORIENTED_EDGE ( 'NONE', *, *, #47642, .T. ) ;
#56701=( GEOMETRIC_REPRESENTATION_CONTEXT ( 3 ) GLOBAL_UNCERTAINTY_ASSIGNED_CONTEXT ( ( #23673 ) ) GLOBAL_UNIT_ASSIGNED_CONTEXT ( ( #33078, #5278, #38036 ) ) REPRESENTATION_CONTEXT ( 'NONE', 'WORKASPACE' ) );
#56708=ADVANCED_FACE ( 'NONE', ( #53196 ), #16279, .T. ) ;
#56710=EDGE_CURVE ( 'NONE', #45813, #42291, #66889, .T. ) ;
#56719=UNCERTAINTY_MEASURE_WITH_UNIT (LENGTH_MEASURE( 1.000000000000000082E-05 ), #57986, 'distance_accuracy_value', 'NONE');
#56804=( NAMED_UNIT ( * ) PLANE_ANGLE_UNIT ( ) SI_UNIT ( $, .RADIAN. ) );
#56830=COLOUR_RGB ( '', 0.40784314, 0.44705882, 0.49803922) ;
#56848=DIRECTION ( 'NONE',  ( 0.07854820085872894764, 0.9914125719358882760, -0.1045528208578022367 ) ) ;
#56876=CARTESIAN_POINT ( 'NONE',  ( 3.999798566743339556, 49.09558629977726696, 2.000000000000000000 ) ) ;
#56884=( NAMED_UNIT ( * ) PLANE_ANGLE_UNIT ( ) SI_UNIT ( $, .RADIAN. ) );
#56925=DIRECTION ( 'NONE',  ( -1.000000000000000000, -1.224646799147353454E-16, 0.000000000000000000 ) ) ;
#56928=ORIENTED_EDGE ( 'NONE', *, *, #5331, .F. ) ;
#56958=ADVANCED_FACE ( 'NONE', ( #29557 ), #67904, .F. ) ;
#56976=EDGE_LOOP ( 'NONE', ( #10441, #14142, #39616, #4152, #65635, #16775 ) ) ;
#57000=AXIS2_PLACEMENT_3D ( 'NONE', #32681, #5252, #26698 ) ;
#57048=VECTOR ( 'NONE', #7987, 1000.000000000000000 ) ;
#57067=ORIENTED_EDGE ( 'NONE', *, *, #3402, .F. ) ;
#57084=DIRECTION ( 'NONE',  ( 0.000000000000000000, 1.350863103983176297E-16, 1.000000000000000000 ) ) ;
#57196=DIRECTION ( 'NONE',  ( -0.000000000000000000, -0.000000000000000000, -1.000000000000000000 ) ) ;
#57221=VECTOR ( 'NONE', #38148, 1000.000000000000114 ) ;
#57289=DIRECTION ( 'NONE',  ( 0.000000000000000000, -0.1048768571002353378, 0.9944852160011111719 ) ) ;
#57295=CARTESIAN_POINT ( 'NONE',  ( 3.999798566743339556, 49.09558629977726696, -2.000000000000000000 ) ) ;
#57298=UNCERTAINTY_MEASURE_WITH_UNIT (LENGTH_MEASURE( 1.000000000000000082E-05 ), #219, 'distance_accuracy_value', 'NONE');
#57307=CARTESIAN_POINT ( 'NONE',  ( -1.953228634907021810, 72.00000000000001421, -6.349999999999997868 ) ) ;
#57327=FILL_AREA_STYLE ('',( #25652 ) ) ;
#57374=MECHANICAL_DESIGN_GEOMETRIC_PRESENTATION_REPRESENTATION('',(#9069),#5625);
#57433=MECHANICAL_DESIGN_GEOMETRIC_PRESENTATION_REPRESENTATION('',(#30433),#45122);
#57608=SURFACE_STYLE_FILL_AREA ( #21011 ) ;
#57654=DIRECTION ( 'NONE',  ( 0.000000000000000000, 0.000000000000000000, 1.000000000000000000 ) ) ;
#57860=CARTESIAN_POINT ( 'NONE',  ( 0.04677136509298115974, 68.99999999999998579, 12.50000000000000000 ) ) ;
#57888=DIRECTION ( 'NONE',  ( 0.000000000000000000, 0.000000000000000000, -1.000000000000000000 ) ) ;
#57986=( LENGTH_UNIT ( ) NAMED_UNIT ( * ) SI_UNIT ( .MILLI., .METRE. ) );
#58020=FACE_OUTER_BOUND ( 'NONE', #21827, .T. ) ;
#58041=STYLED_ITEM ( 'NONE', ( #59488 ), #40379 ) ;
#58085=AXIS2_PLACEMENT_3D ( 'NONE', #68342, #45623, #67039 ) ;
#58261=COLOUR_RGB ( '', 0.72549020, 0.75294118, 0.79215686) ;
#58288=ADVANCED_FACE ( 'NONE', ( #16547 ), #42274, .T. ) ;
#58295=PRESENTATION_STYLE_ASSIGNMENT (( #41116 ) ) ;
#58315=SURFACE_STYLE_USAGE ( .BOTH. , #47108 ) ;
#58323=ORIENTED_EDGE ( 'NONE', *, *, #67094, .T. ) ;
#58346=CARTESIAN_POINT ( 'NONE',  ( -17.41962728626436530, -0.1139526552317604857, 2.000000000000000000 ) ) ;
#58380=DIRECTION ( 'NONE',  ( -0.000000000000000000, -0.000000000000000000, -1.000000000000000000 ) ) ;
#58410=DIRECTION ( 'NONE',  ( -0.3420201433256663814, 0.9396926207859092051, 0.000000000000000000 ) ) ;
#58415=CARTESIAN_POINT ( 'NONE',  ( 1.804495846578303864, 51.08602766979955589, -7.112547338523483198 ) ) ;
#58432=LINE ( 'NONE', #53172, #1716 ) ;
#58491=ORIENTED_EDGE ( 'NONE', *, *, #53084, .F. ) ;
#58530=EDGE_CURVE ( 'NONE', #11115, #47453, #51293, .T. ) ;
#58601=UNCERTAINTY_MEASURE_WITH_UNIT (LENGTH_MEASURE( 1.000000000000000082E-05 ), #50971, 'distance_accuracy_value', 'NONE');
#58682=DIRECTION ( 'NONE',  ( 0.000000000000000000, 0.000000000000000000, 1.000000000000000000 ) ) ;
#58708=SURFACE_STYLE_FILL_AREA ( #65000 ) ;
#58765=CARTESIAN_POINT ( 'NONE',  ( 3.046771365092978190, 72.00000000000001421, 6.349999999999997868 ) ) ;
#58767=SURFACE_SIDE_STYLE ('',( #21474 ) ) ;
#58792=EDGE_CURVE ( 'NONE', #22827, #42596, #3198, .T. ) ;
#58951=EDGE_CURVE ( 'NONE', #43499, #46838, #42711, .T. ) ;
#58960=LINE ( 'NONE', #47773, #52844 ) ;
#59036=AXIS2_PLACEMENT_3D ( 'NONE', #48640, #37753, #64069 ) ;
#59070=DIRECTION ( 'NONE',  ( -1.000000000000000000, 0.000000000000000000, 0.000000000000000000 ) ) ;
#59073=SURFACE_STYLE_USAGE ( .BOTH. , #68960 ) ;
#59304=FILL_AREA_STYLE ('',( #37930 ) ) ;
#59357=VERTEX_POINT ( 'NONE', #67475 ) ;
#59382=( LENGTH_UNIT ( ) NAMED_UNIT ( * ) SI_UNIT ( .MILLI., .METRE. ) );
#59396=CARTESIAN_POINT ( 'NONE',  ( 0.04677136509298115974, 68.99999999999998579, 2.000000000000000000 ) ) ;
#59424=ORIENTED_EDGE ( 'NONE', *, *, #2164, .F. ) ;
#59488=PRESENTATION_STYLE_ASSIGNMENT (( #61714 ) ) ;
#59509=VERTEX_POINT ( 'NONE', #538 ) ;
#59528=FILL_AREA_STYLE ('',( #396 ) ) ;
#59537=VECTOR ( 'NONE', #64676, 1000.000000000000000 ) ;
#59607=( LENGTH_UNIT ( ) NAMED_UNIT ( * ) SI_UNIT ( .MILLI., .METRE. ) );
#59652=ORIENTED_EDGE ( 'NONE', *, *, #44823, .T. ) ;
#59678=ADVANCED_FACE ( 'NONE', ( #58020 ), #31241, .F. ) ;
#59707=DIRECTION ( 'NONE',  ( 0.000000000000000000, 1.350863103983176297E-16, -1.000000000000000000 ) ) ;
#59732=FACE_OUTER_BOUND ( 'NONE', #4819, .T. ) ;
#59800=SURFACE_STYLE_FILL_AREA ( #38398 ) ;
#59818=ORIENTED_EDGE ( 'NONE', *, *, #47772, .T. ) ;
#59891=FILL_AREA_STYLE_COLOUR ( '', #1039 ) ;
#59977=CARTESIAN_POINT ( 'NONE',  ( 0.000000000000000000, 0.000000000000000000, 0.000000000000000000 ) ) ;
#59987=MECHANICAL_DESIGN_GEOMETRIC_PRESENTATION_REPRESENTATION('',(#1540),#61092);
#60014=SURFACE_SIDE_STYLE ('',( #2617 ) ) ;
#60017=UNCERTAINTY_MEASURE_WITH_UNIT (LENGTH_MEASURE( 1.000000000000000082E-05 ), #69621, 'distance_accuracy_value', 'NONE');
#60083=FILL_AREA_STYLE_COLOUR ( '', #6007 ) ;
#60085=ORIENTED_EDGE ( 'NONE', *, *, #34391, .F. ) ;
#60112=( NAMED_UNIT ( * ) PLANE_ANGLE_UNIT ( ) SI_UNIT ( $, .RADIAN. ) );
#60246=( LENGTH_UNIT ( ) NAMED_UNIT ( * ) SI_UNIT ( .MILLI., .METRE. ) );
#60280=ORIENTED_EDGE ( 'NONE', *, *, #64385, .T. ) ;
#60283=ORIENTED_EDGE ( 'NONE', *, *, #2090, .F. ) ;
#60411=CARTESIAN_POINT ( 'NONE',  ( 17.15973193263811680, -3.000000000000000000, 12.50000000000000000 ) ) ;
#60462=PLANE ( 'NONE',  #41422 ) ;
#60566=EDGE_LOOP ( 'NONE', ( #527, #44744, #6698, #41282 ) ) ;
#60568=VERTEX_POINT ( 'NONE', #58346 ) ;
#60633=VECTOR ( 'NONE', #21305, 1000.000000000000227 ) ;
#60753=( GEOMETRIC_REPRESENTATION_CONTEXT ( 3 ) GLOBAL_UNCERTAINTY_ASSIGNED_CONTEXT ( ( #51585 ) ) GLOBAL_UNIT_ASSIGNED_CONTEXT ( ( #22731, #17477, #12859 ) ) REPRESENTATION_CONTEXT ( 'NONE', 'WORKASPACE' ) );
#60757=VERTEX_POINT ( 'NONE', #18565 ) ;
#60796=( GEOMETRIC_REPRESENTATION_CONTEXT ( 3 ) GLOBAL_UNCERTAINTY_ASSIGNED_CONTEXT ( ( #15712 ) ) GLOBAL_UNIT_ASSIGNED_CONTEXT ( ( #60246, #22965, #7126 ) ) REPRESENTATION_CONTEXT ( 'NONE', 'WORKASPACE' ) );
#60797=ORIENTED_EDGE ( 'NONE', *, *, #51397, .F. ) ;
#60814=CARTESIAN_POINT ( 'NONE',  ( 1.804495846578303864, 51.08602766979955589, -2.000000000000000000 ) ) ;
#60828=VECTOR ( 'NONE', #19434, 1000.000000000000000 ) ;
#60842=DIRECTION ( 'NONE',  ( 0.000000000000000000, 0.000000000000000000, -1.000000000000000000 ) ) ;
#60909=SURFACE_STYLE_USAGE ( .BOTH. , #18011 ) ;
#60913=EDGE_CURVE ( 'NONE', #51672, #47453, #38441, .T. ) ;
#60937=CARTESIAN_POINT ( 'NONE',  ( -20.29401227849671230, 1.590180419696184400, 12.33230205742959740 ) ) ;
#60984=AXIS2_PLACEMENT_3D ( 'NONE', #68609, #10211, #69302 ) ;
#61019=( NAMED_UNIT ( * ) SI_UNIT ( $, .STERADIAN. ) SOLID_ANGLE_UNIT ( ) );
#61037=PRESENTATION_STYLE_ASSIGNMENT (( #32944 ) ) ;
#61092=( GEOMETRIC_REPRESENTATION_CONTEXT ( 3 ) GLOBAL_UNCERTAINTY_ASSIGNED_CONTEXT ( ( #67286 ) ) GLOBAL_UNIT_ASSIGNED_CONTEXT ( ( #13781, #2472, #40893 ) ) REPRESENTATION_CONTEXT ( 'NONE', 'WORKASPACE' ) );
#61097=MECHANICAL_DESIGN_GEOMETRIC_PRESENTATION_REPRESENTATION('',(#46603),#63366);
#61158=COLOUR_RGB ( '', 0.31764706, 0.68627451, 0.89019608) ;
#61178=CARTESIAN_POINT ( 'NONE',  ( 3.999798566743339556, 8.867945265733707672, 2.000000000000000000 ) ) ;
#61254=ORIENTED_EDGE ( 'NONE', *, *, #45159, .T. ) ;
#61377=CYLINDRICAL_SURFACE ( 'NONE', #4653, 17.42000000000001236 ) ;
#61388=FILL_AREA_STYLE ('',( #39991 ) ) ;
#61402=CARTESIAN_POINT ( 'NONE',  ( -13.10261986875638129, 54.37406082015609599, -6.765796499695130528 ) ) ;
#61467=CARTESIAN_POINT ( 'NONE',  ( -13.23915246117191025, 52.65078610323165265, 2.000000000000000000 ) ) ;
#61492=FILL_AREA_STYLE_COLOUR ( '', #58261 ) ;
#61542=( LENGTH_UNIT ( ) NAMED_UNIT ( * ) SI_UNIT ( .MILLI., .METRE. ) );
#61714=SURFACE_STYLE_USAGE ( .BOTH. , #40308 ) ;
#61725=SURFACE_STYLE_FILL_AREA ( #14614 ) ;
#61730=CARTESIAN_POINT ( 'NONE',  ( -6.588738478070744975, 51.73049953470015083, -7.044582342571018785 ) ) ;
#61846=CARTESIAN_POINT ( 'NONE',  ( -37.50000000000000000, 58.31681314173471975, 6.349999999999996092 ) ) ;
#61907=DIRECTION ( 'NONE',  ( -1.000000000000000000, -9.811390859391774840E-17, 0.000000000000000000 ) ) ;
#61967=ORIENTED_EDGE ( 'NONE', *, *, #4612, .F. ) ;
#62044=STYLED_ITEM ( 'NONE', ( #36898 ), #19005 ) ;
#62060=PRESENTATION_STYLE_ASSIGNMENT (( #14956 ) ) ;
#62076=MECHANICAL_DESIGN_GEOMETRIC_PRESENTATION_REPRESENTATION('',(#48688),#13793);
#62084=( NAMED_UNIT ( * ) SI_UNIT ( $, .STERADIAN. ) SOLID_ANGLE_UNIT ( ) );
#62090=COLOUR_RGB ( '', 0.40784314, 0.44705882, 0.49803922) ;
#62123=VECTOR ( 'NONE', #42183, 1000.000000000000000 ) ;
#62178=( LENGTH_UNIT ( ) NAMED_UNIT ( * ) SI_UNIT ( .MILLI., .METRE. ) );
#62261=LINE ( 'NONE', #23933, #34020 ) ;
#62263=ORIENTED_EDGE ( 'NONE', *, *, #13410, .F. ) ;
#62283=COLOUR_RGB ( '', 0.40784314, 0.44705882, 0.49803922) ;
#62315=FILL_AREA_STYLE ('',( #24654 ) ) ;
#62317=ADVANCED_FACE ( 'NONE', ( #27547 ), #26523, .T. ) ;
#62432=SURFACE_SIDE_STYLE ('',( #8631 ) ) ;
#62447=FILL_AREA_STYLE_COLOUR ( '', #62090 ) ;
#62515=EDGE_LOOP ( 'NONE', ( #7102, #6404, #58323, #31580, #34365, #33444, #24010, #41881, #66777, #63647, #42587, #38022, #14893 ) ) ;
#62522=LINE ( 'NONE', #62859, #62123 ) ;
#62671=CARTESIAN_POINT ( 'NONE',  ( 3.046771365092978190, 72.00000000000001421, -6.349999999999997868 ) ) ;
#62744=LINE ( 'NONE', #9674, #78 ) ;
#62754=EDGE_CURVE ( 'NONE', #17724, #42390, #15429, .T. ) ;
#62766=CARTESIAN_POINT ( 'NONE',  ( -37.50000000000000000, 83.99999999999998579, -6.349999999999999645 ) ) ;
#62808=ORIENTED_EDGE ( 'NONE', *, *, #37727, .F. ) ;
#62859=CARTESIAN_POINT ( 'NONE',  ( 8.319377385370872346, -3.000000000000000888, -2.000000000000000000 ) ) ;
#62862=EDGE_CURVE ( 'NONE', #43499, #42596, #64954, .T. ) ;
#62887=DIRECTION ( 'NONE',  ( 0.000000000000000000, 0.9944852160011111719, -0.1048768571002353378 ) ) ;
#63146=CIRCLE ( 'NONE', #65407, 20.42000000000000526 ) ;
#63200=PRESENTATION_STYLE_ASSIGNMENT (( #24493 ) ) ;
#63243=AXIS2_PLACEMENT_3D ( 'NONE', #68872, #41453, #24886 ) ;
#63277=CARTESIAN_POINT ( 'NONE',  ( 1.999798566743339334, 49.09558629977726696, 2.000000000000000000 ) ) ;
#63366=( GEOMETRIC_REPRESENTATION_CONTEXT ( 3 ) GLOBAL_UNCERTAINTY_ASSIGNED_CONTEXT ( ( #51819 ) ) GLOBAL_UNIT_ASSIGNED_CONTEXT ( ( #52654, #56884, #9046 ) ) REPRESENTATION_CONTEXT ( 'NONE', 'WORKASPACE' ) );
#63371=ORIENTED_EDGE ( 'NONE', *, *, #58951, .T. ) ;
#63433=MECHANICAL_DESIGN_GEOMETRIC_PRESENTATION_REPRESENTATION('',(#30821),#56701);
#63625=MECHANICAL_DESIGN_GEOMETRIC_PRESENTATION_REPRESENTATION('',(#27642),#65848);
#63647=ORIENTED_EDGE ( 'NONE', *, *, #2230, .T. ) ;
#63718=VERTEX_POINT ( 'NONE', #45395 ) ;
#63721=DIRECTION ( 'NONE',  ( 0.000000000000000000, 1.350863103983176297E-16, 1.000000000000000000 ) ) ;
#63777=( NAMED_UNIT ( * ) PLANE_ANGLE_UNIT ( ) SI_UNIT ( $, .RADIAN. ) );
#63808=UNCERTAINTY_MEASURE_WITH_UNIT (LENGTH_MEASURE( 1.000000000000000082E-05 ), #59382, 'distance_accuracy_value', 'NONE');
#63822=CARTESIAN_POINT ( 'NONE',  ( 8.373843646579334887, 5.621768377696955810, -11.90713709031378897 ) ) ;
#63828=VERTEX_POINT ( 'NONE', #30890 ) ;
#63923=FILL_AREA_STYLE_COLOUR ( '', #17151 ) ;
#64011=EDGE_CURVE ( 'NONE', #11115, #52209, #54003, .T. ) ;
#64069=DIRECTION ( 'NONE',  ( 0.000000000000000000, 0.000000000000000000, 1.000000000000000000 ) ) ;
#64159=( NAMED_UNIT ( * ) PLANE_ANGLE_UNIT ( ) SI_UNIT ( $, .RADIAN. ) );
#64225=CARTESIAN_POINT ( 'NONE',  ( 6.999798566743336004, 53.02677333163759243, -6.907879333238362562 ) ) ;
#64318=UNCERTAINTY_MEASURE_WITH_UNIT (LENGTH_MEASURE( 1.000000000000000082E-05 ), #35349, 'distance_accuracy_value', 'NONE');
#64324=CARTESIAN_POINT ( 'NONE',  ( 1.999798566743339334, 49.09558629977726696, 2.000000000000000000 ) ) ;
#64385=EDGE_CURVE ( 'NONE', #8740, #40876, #58432, .T. ) ;
#64486=DIRECTION ( 'NONE',  ( 1.000000000000000000, 0.000000000000000000, 0.000000000000000000 ) ) ;
#64493=VECTOR ( 'NONE', #1584, 1000.000000000000227 ) ;
#64541=ORIENTED_EDGE ( 'NONE', *, *, #12057, .F. ) ;
#64633=CARTESIAN_POINT ( 'NONE',  ( -10.11618306975752368, 54.14354156754873060, 2.000000000000000000 ) ) ;
#64666=STYLED_ITEM ( 'NONE', ( #20387 ), #56958 ) ;
#64676=DIRECTION ( 'NONE',  ( -0.000000000000000000, -0.000000000000000000, -1.000000000000000000 ) ) ;
#64686=ORIENTED_EDGE ( 'NONE', *, *, #51397, .T. ) ;
#64699=( BOUNDED_CURVE ( )  B_SPLINE_CURVE ( 3, ( #23260, #6376, #27804, #18339 ),
 .UNSPECIFIED., .F., .F. ) 
 B_SPLINE_CURVE_WITH_KNOTS ( ( 4, 4 ),
 ( 3.043785426622117374, 4.712388980384689674 ),
 .UNSPECIFIED. ) 
 CURVE ( )  GEOMETRIC_REPRESENTATION_ITEM ( )  RATIONAL_B_SPLINE_CURVE ( ( 1.000000000000000000, 0.7811300729168891843, 0.7811300729168891843, 1.000000000000000000 ) ) 
 REPRESENTATION_ITEM ( '' )  );
#64707=( NAMED_UNIT ( * ) SI_UNIT ( $, .STERADIAN. ) SOLID_ANGLE_UNIT ( ) );
#64711=FACE_OUTER_BOUND ( 'NONE', #56280, .T. ) ;
#64774=SURFACE_STYLE_FILL_AREA ( #43383 ) ;
#64881=ADVANCED_FACE ( 'NONE', ( #65657 ), #38627, .F. ) ;
#64887=FILL_AREA_STYLE_COLOUR ( '', #32431 ) ;
#64947=CARTESIAN_POINT ( 'NONE',  ( -10.11618306975752368, 54.14354156754873060, -6.790106699912857202 ) ) ;
#64954=LINE ( 'NONE', #28700, #56603 ) ;
#65000=FILL_AREA_STYLE ('',( #60083 ) ) ;
#65017=VECTOR ( 'NONE', #28628, 1000.000000000000227 ) ;
#65043=VECTOR ( 'NONE', #67062, 1000.000000000000000 ) ;
#65051=VECTOR ( 'NONE', #20584, 1000.000000000000000 ) ;
#65062=PLANE ( 'NONE',  #23606 ) ;
#65203=MECHANICAL_DESIGN_GEOMETRIC_PRESENTATION_REPRESENTATION('',(#36010),#40542);
#65221=ORIENTED_EDGE ( 'NONE', *, *, #32139, .F. ) ;
#65254=CARTESIAN_POINT ( 'NONE',  ( 6.999798566743344885, 8.428680263886673385E-16, 12.50000000000000000 ) ) ;
#65407=AXIS2_PLACEMENT_3D ( 'NONE', #7719, #38408, #7033 ) ;
#65422=FACE_OUTER_BOUND ( 'NONE', #62515, .T. ) ;
#65512=MECHANICAL_DESIGN_GEOMETRIC_PRESENTATION_REPRESENTATION('',(#22850),#2549);
#65517=SHAPE_REPRESENTATION_RELATIONSHIP ( 'NONE' , 'NONE' ,  #31597, #53933 ) ;
#65520=MECHANICAL_DESIGN_GEOMETRIC_PRESENTATION_REPRESENTATION('',(#5965),#16148);
#65542=FACE_OUTER_BOUND ( 'NONE', #10043, .T. ) ;
#65566=VECTOR ( 'NONE', #47083, 1000.000000000000114 ) ;
#65595=SURFACE_STYLE_USAGE ( .BOTH. , #38573 ) ;
#65635=ORIENTED_EDGE ( 'NONE', *, *, #45318, .F. ) ;
#65657=FACE_OUTER_BOUND ( 'NONE', #8790, .T. ) ;
#65728=ORIENTED_EDGE ( 'NONE', *, *, #8105, .F. ) ;
#65784=UNCERTAINTY_MEASURE_WITH_UNIT (LENGTH_MEASURE( 1.000000000000000082E-05 ), #43026, 'distance_accuracy_value', 'NONE');
#65848=( GEOMETRIC_REPRESENTATION_CONTEXT ( 3 ) GLOBAL_UNCERTAINTY_ASSIGNED_CONTEXT ( ( #54435 ) ) GLOBAL_UNIT_ASSIGNED_CONTEXT ( ( #33642, #11843, #38974 ) ) REPRESENTATION_CONTEXT ( 'NONE', 'WORKASPACE' ) );
#65974=FILL_AREA_STYLE ('',( #511 ) ) ;
#65983=SURFACE_STYLE_USAGE ( .BOTH. , #60014 ) ;
#66121=DIRECTION ( 'NONE',  ( 1.000000000000000000, 0.000000000000000000, 0.000000000000000000 ) ) ;
#66136=EDGE_LOOP ( 'NONE', ( #47803, #60797, #48661 ) ) ;
#66317=ORIENTED_EDGE ( 'NONE', *, *, #46685, .T. ) ;
#66409=PRESENTATION_STYLE_ASSIGNMENT (( #5928 ) ) ;
#66432=( BOUNDED_CURVE ( )  B_SPLINE_CURVE ( 3, ( #24130, #61402, #34674, #23783 ),
 .UNSPECIFIED., .F., .F. ) 
 B_SPLINE_CURVE_WITH_KNOTS ( ( 4, 4 ),
 ( 1.649859741910239874, 3.741551587622924835 ),
 .UNSPECIFIED. ) 
 CURVE ( )  GEOMETRIC_REPRESENTATION_ITEM ( )  RATIONAL_B_SPLINE_CURVE ( ( 1.000000000000000000, 0.6674467249320013007, 0.6674467249320013007, 1.000000000000000000 ) ) 
 REPRESENTATION_ITEM ( '' )  );
#66470=DIRECTION ( 'NONE',  ( 1.000000000000000000, 0.000000000000000000, 0.000000000000000000 ) ) ;
#66530=UNCERTAINTY_MEASURE_WITH_UNIT (LENGTH_MEASURE( 1.000000000000000082E-05 ), #56585, 'distance_accuracy_value', 'NONE');
#66684=FACE_BOUND ( 'NONE', #9741, .T. ) ;
#66690=PLANE ( 'NONE',  #58085 ) ;
#66744=CARTESIAN_POINT ( 'NONE',  ( 3.999798566743338668, 49.09558629977726696, -7.322456175549363344 ) ) ;
#66777=ORIENTED_EDGE ( 'NONE', *, *, #67748, .T. ) ;
#66786=FACE_OUTER_BOUND ( 'NONE', #56976, .T. ) ;
#66799=CARTESIAN_POINT ( 'NONE',  ( 3.062509476195515228E-31, -2.500728763858896269E-15, 12.50000000000000000 ) ) ;
#66835=LINE ( 'NONE', #8772, #2308 ) ;
#66889=CIRCLE ( 'NONE', #35445, 17.99999999999999645 ) ;
#66913=DIRECTION ( 'NONE',  ( 0.3420201433256663814, -0.9396926207859092051, 0.000000000000000000 ) ) ;
#66964=EDGE_CURVE ( 'NONE', #9321, #42390, #47586, .T. ) ;
#67013=DIRECTION ( 'NONE',  ( 1.000000000000000000, 0.000000000000000000, 0.000000000000000000 ) ) ;
#67021=CARTESIAN_POINT ( 'NONE',  ( -13.23915246117191025, 52.65078610323165265, -2.000000000000000000 ) ) ;
#67039=DIRECTION ( 'NONE',  ( -0.3420201433256663814, 0.9396926207859092051, 0.000000000000000000 ) ) ;
#67062=DIRECTION ( 'NONE',  ( -0.000000000000000000, -0.000000000000000000, 1.000000000000000000 ) ) ;
#67094=EDGE_CURVE ( 'NONE', #69289, #18031, #41237, .T. ) ;
#67111=APPLICATION_CONTEXT ( 'automotive_design' ) ;
#67219=VECTOR ( 'NONE', #55903, 1000.000000000000000 ) ;
#67220=( NAMED_UNIT ( * ) PLANE_ANGLE_UNIT ( ) SI_UNIT ( $, .RADIAN. ) );
#67239=DIRECTION ( 'NONE',  ( 0.000000000000000000, 1.350863103983176297E-16, -1.000000000000000000 ) ) ;
#67286=UNCERTAINTY_MEASURE_WITH_UNIT (LENGTH_MEASURE( 1.000000000000000082E-05 ), #13781, 'distance_accuracy_value', 'NONE');
#67360=FACE_OUTER_BOUND ( 'NONE', #29511, .T. ) ;
#67390=LINE ( 'NONE', #35397, #38786 ) ;
#67436=ORIENTED_EDGE ( 'NONE', *, *, #8185, .F. ) ;
#67455=LINE ( 'NONE', #61467, #27757 ) ;
#67461=PRESENTATION_STYLE_ASSIGNMENT (( #29107 ) ) ;
#67475=CARTESIAN_POINT ( 'NONE',  ( 8.319377385370872346, -3.000000000000000888, 12.50000000000000000 ) ) ;
#67476=ORIENTED_EDGE ( 'NONE', *, *, #41274, .T. ) ;
#67594=CARTESIAN_POINT ( 'NONE',  ( -37.50000000000000000, 83.99999999999998579, 6.349999999999999645 ) ) ;
#67684=AXIS2_PLACEMENT_3D ( 'NONE', #68693, #52184, #2874 ) ;
#67748=EDGE_CURVE ( 'NONE', #3437, #18730, #39166, .T. ) ;
#67816=ORIENTED_EDGE ( 'NONE', *, *, #10653, .F. ) ;
#67821=( LENGTH_UNIT ( ) NAMED_UNIT ( * ) SI_UNIT ( .MILLI., .METRE. ) );
#67866=CARTESIAN_POINT ( 'NONE',  ( -37.50000000000000000, 58.31681314173471975, -6.349999999999996092 ) ) ;
#67904=PLANE ( 'NONE',  #52331 ) ;
#68019=ORIENTED_EDGE ( 'NONE', *, *, #10725, .T. ) ;
#68078=( LENGTH_UNIT ( ) NAMED_UNIT ( * ) SI_UNIT ( .MILLI., .METRE. ) );
#68087=( GEOMETRIC_REPRESENTATION_CONTEXT ( 3 ) GLOBAL_UNCERTAINTY_ASSIGNED_CONTEXT ( ( #55211 ) ) GLOBAL_UNIT_ASSIGNED_CONTEXT ( ( #26364, #22137, #37328 ) ) REPRESENTATION_CONTEXT ( 'NONE', 'WORKASPACE' ) );
#68152=ORIENTED_EDGE ( 'NONE', *, *, #42457, .F. ) ;
#68155=ADVANCED_FACE ( 'NONE', ( #65422 ), #60462, .F. ) ;
#68242=ORIENTED_EDGE ( 'NONE', *, *, #51949, .T. ) ;
#68342=CARTESIAN_POINT ( 'NONE',  ( 3.999798566743339556, 8.867945265733707672, 2.000000000000000000 ) ) ;
#68397=ORIENTED_EDGE ( 'NONE', *, *, #15691, .T. ) ;
#68399=( NAMED_UNIT ( * ) SI_UNIT ( $, .STERADIAN. ) SOLID_ANGLE_UNIT ( ) );
#68418=CARTESIAN_POINT ( 'NONE',  ( -13.10261986875638129, 54.37406082015609599, 6.765796499695130528 ) ) ;
#68425=UNCERTAINTY_MEASURE_WITH_UNIT (LENGTH_MEASURE( 1.000000000000000082E-05 ), #34656, 'distance_accuracy_value', 'NONE');
#68474=AXIS2_PLACEMENT_3D ( 'NONE', #31764, #53253, #69415 ) ;
#68482=FACE_OUTER_BOUND ( 'NONE', #22793, .T. ) ;
#68516=ORIENTED_EDGE ( 'NONE', *, *, #28974, .T. ) ;
#68537=CARTESIAN_POINT ( 'NONE',  ( 3.999798566743339556, 49.09558629977726696, 2.000000000000000000 ) ) ;
#68609=CARTESIAN_POINT ( 'NONE',  ( 0.000000000000000000, 0.000000000000000000, 12.50000000000000000 ) ) ;
#68672=ORIENTED_EDGE ( 'NONE', *, *, #33871, .T. ) ;
#68693=CARTESIAN_POINT ( 'NONE',  ( -11.24540022918535698, 52.49282396394303873, 2.000000000000000000 ) ) ;
#68872=CARTESIAN_POINT ( 'NONE',  ( 6.999798566743344885, 7.519018533394457353E-16, 12.50000000000000000 ) ) ;
#68945=VECTOR ( 'NONE', #8727, 1000.000000000000000 ) ;
#68960=SURFACE_SIDE_STYLE ('',( #10892 ) ) ;
#69026=DIRECTION ( 'NONE',  ( 1.000000000000000000, 0.000000000000000000, 0.000000000000000000 ) ) ;
#69116=ORIENTED_EDGE ( 'NONE', *, *, #17200, .F. ) ;
#69182=CARTESIAN_POINT ( 'NONE',  ( 10.57623092156537936, 58.31681314173471975, -6.349999999999996092 ) ) ;
#69217=( GEOMETRIC_REPRESENTATION_CONTEXT ( 3 ) GLOBAL_UNCERTAINTY_ASSIGNED_CONTEXT ( ( #60017 ) ) GLOBAL_UNIT_ASSIGNED_CONTEXT ( ( #69621, #52780, #64707 ) ) REPRESENTATION_CONTEXT ( 'NONE', 'WORKASPACE' ) );
#69289=VERTEX_POINT ( 'NONE', #47485 ) ;
#69302=DIRECTION ( 'NONE',  ( 1.000000000000000000, 0.000000000000000000, 0.000000000000000000 ) ) ;
#69365=VERTEX_POINT ( 'NONE', #10840 ) ;
#69415=DIRECTION ( 'NONE',  ( -1.000000000000000000, 0.000000000000000000, 0.000000000000000000 ) ) ;
#69568=EDGE_CURVE ( 'NONE', #60568, #69365, #24749, .T. ) ;
#69581=VECTOR ( 'NONE', #31115, 1000.000000000000000 ) ;
#69620=CARTESIAN_POINT ( 'NONE',  ( 8.319377385370872346, -3.000000000000000888, 2.000000000000000000 ) ) ;
#69621=( LENGTH_UNIT ( ) NAMED_UNIT ( * ) SI_UNIT ( .MILLI., .METRE. ) );
ENDSEC;
END-ISO-10303-21;
